ISO-10303-21;
HEADER;
FILE_DESCRIPTION (('STEP AP214'),
    '1' );
FILE_NAME ('Lock Lever.step',
    '2026-10-23T18:01:19',
    ( '' ),
    ( '' ),
    'SwSTEP 2.0',
    'SolidWorks 2025',
    '' );
FILE_SCHEMA (( 'AUTOMOTIVE_DESIGN' ));
ENDSEC;

DATA;
#6=MECHANICAL_DESIGN_GEOMETRIC_PRESENTATION_REPRESENTATION('',(#7130),#10291);
#8=EDGE_LOOP ( 'NONE', ( #3348, #3892, #6424, #10315, #10248, #3759, #9875, #3838 ) ) ;
#23=AXIS2_PLACEMENT_3D ( 'NONE', #11429, #932, #7837 ) ;
#24=DIRECTION ( 'NONE',  ( 0.000000000000000000, 0.000000000000000000, -1.000000000000000000 ) ) ;
#44=DIRECTION ( 'NONE',  ( 0.000000000000000000, 0.000000000000000000, -1.000000000000000000 ) ) ;
#57=CARTESIAN_POINT ( 'NONE',  ( 0.1007315414569005807, 0.000000000000000000, -0.7936328852534507705 ) ) ;
#61=PLANE ( 'NONE',  #8465 ) ;
#79=FACE_OUTER_BOUND ( 'NONE', #9861, .T. ) ;
#93=DIRECTION ( 'NONE',  ( -0.000000000000000000, -1.000000000000000000, -0.000000000000000000 ) ) ;
#99=CARTESIAN_POINT ( 'NONE',  ( 0.4125000000000000333, 0.1749999999999999889, 0.3724999999999999978 ) ) ;
#100=AXIS2_PLACEMENT_3D ( 'NONE', #9537, #4707, #14178 ) ;
#102=DIRECTION ( 'NONE',  ( 0.000000000000000000, 1.000000000000000000, -0.000000000000000000 ) ) ;
#108=CIRCLE ( 'NONE', #2074, 0.03999999999999998002 ) ;
#140=EDGE_LOOP ( 'NONE', ( #8999, #12949, #3584, #329, #10455, #10394, #1093, #10887, #312, #1729, #3941 ) ) ;
#143=PLANE ( 'NONE',  #5754 ) ;
#146=ORIENTED_EDGE ( 'NONE', *, *, #13885, .T. ) ;
#164=CARTESIAN_POINT ( 'NONE',  ( -0.3724999999999999423, 0.1749999999999999889, 0.3724999999999999978 ) ) ;
#204=CARTESIAN_POINT ( 'NONE',  ( 0.4193347797797013499, 0.1749999999999999889, -1.564978703518711711 ) ) ;
#211=ORIENTED_EDGE ( 'NONE', *, *, #10111, .F. ) ;
#213=VECTOR ( 'NONE', #1409, 39.37007874015748143 ) ;
#223=ORIENTED_EDGE ( 'NONE', *, *, #6094, .T. ) ;
#227=CARTESIAN_POINT ( 'NONE',  ( 0.7936328852534488831, 0.1749999999999999889, -0.1007315414569159018 ) ) ;
#244=ORIENTED_EDGE ( 'NONE', *, *, #5155, .F. ) ;
#260=EDGE_CURVE ( 'NONE', #10245, #11406, #12148, .T. ) ;
#312=ORIENTED_EDGE ( 'NONE', *, *, #6259, .T. ) ;
#321=( CONVERSION_BASED_UNIT ( 'INCH', #9691 ) LENGTH_UNIT ( ) NAMED_UNIT ( #8723 ) );
#329=ORIENTED_EDGE ( 'NONE', *, *, #1473, .T. ) ;
#347=AXIS2_PLACEMENT_3D ( 'NONE', #11254, #8885, #14698 ) ;
#360=EDGE_LOOP ( 'NONE', ( #2788, #10549, #4637, #1852 ) ) ;
#367=DIRECTION ( 'NONE',  ( -0.000000000000000000, -1.000000000000000000, -0.000000000000000000 ) ) ;
#374=ORIENTED_EDGE ( 'NONE', *, *, #6094, .F. ) ;
#409=AXIS2_PLACEMENT_3D ( 'NONE', #164, #4937, #14245 ) ;
#447=FACE_OUTER_BOUND ( 'NONE', #360, .T. ) ;
#472=FACE_OUTER_BOUND ( 'NONE', #6050, .T. ) ;
#492=AXIS2_PLACEMENT_3D ( 'NONE', #3318, #11420, #3396 ) ;
#514=CARTESIAN_POINT ( 'NONE',  ( 0.5400755080658357077, 0.1749999999999999889, -1.657626322880899616 ) ) ;
#517=CARTESIAN_POINT ( 'NONE',  ( -0.4124999999999999223, 0.1749999999999999889, 0.3724999999999999978 ) ) ;
#532=EDGE_CURVE ( 'NONE', #2140, #9681, #11301, .T. ) ;
#534=DIRECTION ( 'NONE',  ( 0.000000000000000000, 1.000000000000000000, 0.000000000000000000 ) ) ;
#562=LINE ( 'NONE', #7784, #9750 ) ;
#585=LINE ( 'NONE', #514, #7696 ) ;
#603=VECTOR ( 'NONE', #10639, 39.37007874015748143 ) ;
#616=VERTEX_POINT ( 'NONE', #7829 ) ;
#666=FACE_OUTER_BOUND ( 'NONE', #1064, .T. ) ;
#685=DIRECTION ( 'NONE',  ( 8.659560562354984627E-17, 0.7071067811865432429, -0.7071067811865516806 ) ) ;
#689=ORIENTED_EDGE ( 'NONE', *, *, #4932, .F. ) ;
#702=CARTESIAN_POINT ( 'NONE',  ( 0.3725000000000000533, 0.000000000000000000, 0.4124999999999999778 ) ) ;
#720=CARTESIAN_POINT ( 'NONE',  ( 0.8999999999999998002, 0.1549999999999996103, -0.2949999999999999289 ) ) ;
#742=DIRECTION ( 'NONE',  ( 0.000000000000000000, 0.000000000000000000, -1.000000000000000000 ) ) ;
#743=ADVANCED_FACE ( 'NONE', ( #14005 ), #12943, .T. ) ;
#751=CARTESIAN_POINT ( 'NONE',  ( 1.650520655410188775, 0.000000000000000000, -0.5816197779170857451 ) ) ;
#760=DIRECTION ( 'NONE',  ( 0.000000000000000000, 1.000000000000000000, 0.000000000000000000 ) ) ;
#767=ORIENTED_EDGE ( 'NONE', *, *, #10111, .T. ) ;
#770=PRODUCT_DEFINITION_SHAPE ( 'NONE', 'NONE',  #6322 ) ;
#773=VECTOR ( 'NONE', #11928, 39.37007874015748143 ) ;
#781=ORIENTED_EDGE ( 'NONE', *, *, #14687, .T. ) ;
#784=DIRECTION ( 'NONE',  ( -0.000000000000000000, -1.000000000000000000, -0.000000000000000000 ) ) ;
#888=ORIENTED_EDGE ( 'NONE', *, *, #2012, .T. ) ;
#922=ADVANCED_FACE ( 'NONE', ( #1460 ), #7370, .F. ) ;
#930=AXIS2_PLACEMENT_3D ( 'NONE', #1529, #367, #7504 ) ;
#932=DIRECTION ( 'NONE',  ( -0.000000000000000000, -1.000000000000000000, -0.000000000000000000 ) ) ;
#939=ADVANCED_FACE ( 'NONE', ( #447 ), #5148, .T. ) ;
#965=ORIENTED_EDGE ( 'NONE', *, *, #1473, .F. ) ;
#972=DIRECTION ( 'NONE',  ( -0.000000000000000000, -1.000000000000000000, 0.000000000000000000 ) ) ;
#1040=VERTEX_POINT ( 'NONE', #7133 ) ;
#1042=DIRECTION ( 'NONE',  ( 1.000000000000000000, 0.000000000000000000, 0.000000000000000000 ) ) ;
#1054=CARTESIAN_POINT ( 'NONE',  ( -0.4124999999999999223, 0.000000000000000000, -0.4124999999999999778 ) ) ;
#1060=PLANE ( 'NONE',  #1361 ) ;
#1064=EDGE_LOOP ( 'NONE', ( #12205, #10313, #3455, #7403 ) ) ;
#1093=ORIENTED_EDGE ( 'NONE', *, *, #2010, .T. ) ;
#1102=FACE_OUTER_BOUND ( 'NONE', #10925, .T. ) ;
#1147=AXIS2_PLACEMENT_3D ( 'NONE', #11675, #1178, #24 ) ;
#1159=CARTESIAN_POINT ( 'NONE',  ( 9.797174393178826150E-17, 0.000000000000000000, 0.8000000000000000444 ) ) ;
#1178=DIRECTION ( 'NONE',  ( 0.000000000000000000, 1.000000000000000000, 0.000000000000000000 ) ) ;
#1203=AXIS2_PLACEMENT_3D ( 'NONE', #6983, #7973, #11644 ) ;
#1215=AXIS2_PLACEMENT_3D ( 'NONE', #2597, #6125, #8354 ) ;
#1233=EDGE_LOOP ( 'NONE', ( #7766, #3078, #5605, #10462 ) ) ;
#1257=EDGE_CURVE ( 'NONE', #8991, #4134, #5598, .T. ) ;
#1264=ORIENTED_EDGE ( 'NONE', *, *, #5714, .F. ) ;
#1280=DIRECTION ( 'NONE',  ( 0.000000000000000000, 0.000000000000000000, -1.000000000000000000 ) ) ;
#1294=CYLINDRICAL_SURFACE ( 'NONE', #6715, 0.1250000000000000278 ) ;
#1313=VERTEX_POINT ( 'NONE', #517 ) ;
#1326=DIRECTION ( 'NONE',  ( 3.824587191129971267E-15, 0.000000000000000000, -1.000000000000000000 ) ) ;
#1336=CIRCLE ( 'NONE', #13781, 0.1050000000000006622 ) ;
#1361=AXIS2_PLACEMENT_3D ( 'NONE', #4299, #12538, #3222 ) ;
#1366=ORIENTED_EDGE ( 'NONE', *, *, #12214, .F. ) ;
#1399=ORIENTED_EDGE ( 'NONE', *, *, #6616, .F. ) ;
#1409=DIRECTION ( 'NONE',  ( -0.000000000000000000, 1.000000000000000000, -0.000000000000000000 ) ) ;
#1424=ORIENTED_EDGE ( 'NONE', *, *, #2865, .F. ) ;
#1429=AXIS2_PLACEMENT_3D ( 'NONE', #10033, #7649, #14691 ) ;
#1436=CIRCLE ( 'NONE', #10003, 0.08500000000000004774 ) ;
#1454=FACE_BOUND ( 'NONE', #14206, .T. ) ;
#1460=FACE_OUTER_BOUND ( 'NONE', #5577, .T. ) ;
#1473=EDGE_CURVE ( 'NONE', #10245, #5661, #11168, .T. ) ;
#1478=ORIENTED_EDGE ( 'NONE', *, *, #6197, .F. ) ;
#1486=CARTESIAN_POINT ( 'NONE',  ( 0.8999999999999998002, 0.1549999999999996103, -0.3799999999999999489 ) ) ;
#1488=DIRECTION ( 'NONE',  ( 0.000000000000000000, 0.000000000000000000, -1.000000000000000000 ) ) ;
#1521=DIRECTION ( 'NONE',  ( 1.000000000000000000, 0.000000000000000000, 0.000000000000000000 ) ) ;
#1528=CARTESIAN_POINT ( 'NONE',  ( 0.5400755080658357077, 0.000000000000000000, -1.657626322880899616 ) ) ;
#1529=CARTESIAN_POINT ( 'NONE',  ( 0.000000000000000000, 0.1749999999999999889, 0.000000000000000000 ) ) ;
#1558=APPLICATION_CONTEXT ( 'automotive_design' ) ;
#1565=DIMENSIONAL_EXPONENTS ( 1.000000000000000000, 0.000000000000000000, 0.000000000000000000, 0.000000000000000000, 0.000000000000000000, 0.000000000000000000, 0.000000000000000000 ) ;
#1577=EDGE_CURVE ( 'NONE', #15129, #2976, #12694, .T. ) ;
#1633=ADVANCED_FACE ( 'NONE', ( #10328 ), #4000, .T. ) ;
#1634=CARTESIAN_POINT ( 'NONE',  ( 0.000000000000000000, 0.000000000000000000, 0.000000000000000000 ) ) ;
#1658=DIRECTION ( 'NONE',  ( 0.000000000000000000, 0.000000000000000000, -1.000000000000000000 ) ) ;
#1664=VECTOR ( 'NONE', #9359, 39.37007874015748143 ) ;
#1704=FACE_OUTER_BOUND ( 'NONE', #5355, .T. ) ;
#1729=ORIENTED_EDGE ( 'NONE', *, *, #5239, .T. ) ;
#1745=CARTESIAN_POINT ( 'NONE',  ( 0.000000000000000000, 0.000000000000000000, 0.000000000000000000 ) ) ;
#1749=DIRECTION ( 'NONE',  ( -0.000000000000000000, -1.000000000000000000, -0.000000000000000000 ) ) ;
#1779=CYLINDRICAL_SURFACE ( 'NONE', #23, 0.8000000000000000444 ) ;
#1786=ORIENTED_EDGE ( 'NONE', *, *, #7425, .F. ) ;
#1805=ORIENTED_EDGE ( 'NONE', *, *, #13885, .F. ) ;
#1817=CIRCLE ( 'NONE', #12811, 0.8000000000000000444 ) ;
#1852=ORIENTED_EDGE ( 'NONE', *, *, #4932, .T. ) ;
#1865=VERTEX_POINT ( 'NONE', #7896 ) ;
#1919=AXIS2_PLACEMENT_3D ( 'NONE', #12528, #11247, #742 ) ;
#1951=ORIENTED_EDGE ( 'NONE', *, *, #12872, .F. ) ;
#1987=CARTESIAN_POINT ( 'NONE',  ( -0.3724999999999999423, 0.000000000000000000, -0.4124999999999999778 ) ) ;
#1994=DIRECTION ( 'NONE',  ( 0.000000000000000000, 0.000000000000000000, 1.000000000000000000 ) ) ;
#2000=ORIENTED_EDGE ( 'NONE', *, *, #12278, .F. ) ;
#2010=EDGE_CURVE ( 'NONE', #3074, #2140, #14370, .T. ) ;
#2012=EDGE_CURVE ( 'NONE', #6058, #13458, #8301, .T. ) ;
#2021=EDGE_CURVE ( 'NONE', #4636, #8991, #5843, .T. ) ;
#2044=FACE_OUTER_BOUND ( 'NONE', #14825, .T. ) ;
#2074=AXIS2_PLACEMENT_3D ( 'NONE', #14602, #5434, #2982 ) ;
#2115=ORIENTED_EDGE ( 'NONE', *, *, #12591, .F. ) ;
#2125=EDGE_CURVE ( 'NONE', #6934, #2859, #6142, .T. ) ;
#2140=VERTEX_POINT ( 'NONE', #6063 ) ;
#2150=CARTESIAN_POINT ( 'NONE',  ( 0.3725000000000000533, 0.000000000000000000, 0.4124999999999999778 ) ) ;
#2161=ADVANCED_FACE ( 'NONE', ( #2694 ), #10732, .T. ) ;
#2202=ORIENTED_EDGE ( 'NONE', *, *, #6153, .T. ) ;
#2204=( CONVERSION_BASED_UNIT ( 'INCH', #15136 ) LENGTH_UNIT ( ) NAMED_UNIT ( #1565 ) );
#2248=EDGE_CURVE ( 'NONE', #11406, #13592, #7317, .T. ) ;
#2250=EDGE_CURVE ( 'NONE', #10691, #14656, #2670, .T. ) ;
#2288=CARTESIAN_POINT ( 'NONE',  ( 0.9176380235743000213, 0.1749999999999999889, -0.1164708448095589793 ) ) ;
#2307=EDGE_CURVE ( 'NONE', #7601, #7622, #8047, .T. ) ;
#2341=ADVANCED_FACE ( 'NONE', ( #666 ), #7798, .F. ) ;
#2343=ORIENTED_EDGE ( 'NONE', *, *, #12948, .T. ) ;
#2344=CARTESIAN_POINT ( 'NONE',  ( -0.4124999999999999223, 0.000000000000000000, 0.3724999999999999978 ) ) ;
#2380=VERTEX_POINT ( 'NONE', #3364 ) ;
#2387=DIRECTION ( 'NONE',  ( 0.000000000000000000, -0.000000000000000000, -1.000000000000000000 ) ) ;
#2423=CYLINDRICAL_SURFACE ( 'NONE', #4885, 0.8000000000000000444 ) ;
#2427=LINE ( 'NONE', #99, #213 ) ;
#2456=DIRECTION ( 'NONE',  ( -0.000000000000000000, -1.000000000000000000, 0.000000000000000000 ) ) ;
#2467=DIRECTION ( 'NONE',  ( 0.000000000000000000, 1.000000000000000000, 0.000000000000000000 ) ) ;
#2481=DIRECTION ( 'NONE',  ( -0.2588190451024959260, 0.000000000000000000, 0.9659258262890748625 ) ) ;
#2520=CARTESIAN_POINT ( 'NONE',  ( -0.3724999999999999423, 0.000000000000000000, 0.3724999999999999978 ) ) ;
#2540=CIRCLE ( 'NONE', #6947, 0.1249999999999999861 ) ;
#2552=EDGE_LOOP ( 'NONE', ( #13847, #13027, #9844, #2000 ) ) ;
#2562=CARTESIAN_POINT ( 'NONE',  ( -0.4124999999999999223, 0.1749999999999999889, -0.3724999999999999978 ) ) ;
#2570=ORIENTED_EDGE ( 'NONE', *, *, #6153, .F. ) ;
#2573=VECTOR ( 'NONE', #2481, 39.37007874015748854 ) ;
#2586=LINE ( 'NONE', #3501, #13576 ) ;
#2593=ADVANCED_FACE ( 'NONE', ( #11854 ), #9780, .F. ) ;
#2597=CARTESIAN_POINT ( 'NONE',  ( 0.9176380235743000213, 0.1749999999999999889, -0.1164708448095589793 ) ) ;
#2624=ORIENTED_EDGE ( 'NONE', *, *, #12278, .T. ) ;
#2628=VECTOR ( 'NONE', #93, 39.37007874015748143 ) ;
#2638=ADVANCED_FACE ( 'NONE', ( #10087 ), #10016, .T. ) ;
#2670=CIRCLE ( 'NONE', #15119, 0.8000000000000000444 ) ;
#2686=AXIS2_PLACEMENT_3D ( 'NONE', #14325, #8531, #3860 ) ;
#2689=CARTESIAN_POINT ( 'NONE',  ( 0.1164708448095412852, 0.1749999999999999889, -0.9176380235743023528 ) ) ;
#2694=FACE_OUTER_BOUND ( 'NONE', #10464, .T. ) ;
#2721=ADVANCED_FACE ( 'NONE', ( #14584 ), #11374, .F. ) ;
#2743=DIRECTION ( 'NONE',  ( -0.000000000000000000, -1.000000000000000000, 0.000000000000000000 ) ) ;
#2765=VECTOR ( 'NONE', #14269, 39.37007874015748143 ) ;
#2779=VECTOR ( 'NONE', #3299, 39.37007874015748143 ) ;
#2788=ORIENTED_EDGE ( 'NONE', *, *, #13561, .T. ) ;
#2814=DIRECTION ( 'NONE',  ( -0.000000000000000000, -1.000000000000000000, 0.000000000000000000 ) ) ;
#2818=CIRCLE ( 'NONE', #347, 1.749999999999999556 ) ;
#2851=CARTESIAN_POINT ( 'NONE',  ( 0.8999999999999998002, 0.1549999999999996103, -0.4650000000000000244 ) ) ;
#2859=VERTEX_POINT ( 'NONE', #2562 ) ;
#2865=EDGE_CURVE ( 'NONE', #6548, #1865, #13545, .T. ) ;
#2879=VECTOR ( 'NONE', #685, 39.37007874015748854 ) ;
#2881=CARTESIAN_POINT ( 'NONE',  ( 0.7936328852534487721, 0.1749999999999999889, -0.1007315414569158740 ) ) ;
#2895=DIRECTION ( 'NONE',  ( -0.000000000000000000, -1.000000000000000000, 0.000000000000000000 ) ) ;
#2896=EDGE_LOOP ( 'NONE', ( #8452, #6111, #9278, #9671 ) ) ;
#2908=VERTEX_POINT ( 'NONE', #3864 ) ;
#2950=ORIENTED_EDGE ( 'NONE', *, *, #5888, .T. ) ;
#2976=VERTEX_POINT ( 'NONE', #6381 ) ;
#2978=( LENGTH_UNIT ( ) NAMED_UNIT ( * ) SI_UNIT ( $, .METRE. ) );
#2982=DIRECTION ( 'NONE',  ( 0.000000000000000000, 0.000000000000000000, -1.000000000000000000 ) ) ;
#3021=DIRECTION ( 'NONE',  ( 0.000000000000000000, 1.000000000000000000, 0.000000000000000000 ) ) ;
#3023=( GEOMETRIC_REPRESENTATION_CONTEXT ( 3 ) GLOBAL_UNCERTAINTY_ASSIGNED_CONTEXT ( ( #7100 ) ) GLOBAL_UNIT_ASSIGNED_CONTEXT ( ( #2204, #14049, #3505 ) ) REPRESENTATION_CONTEXT ( 'NONE', 'WORKASPACE' ) );
#3045=CARTESIAN_POINT ( 'NONE',  ( 0.5400755080658357077, 0.1749999999999999889, -1.657626322880899616 ) ) ;
#3047=EDGE_CURVE ( 'NONE', #1040, #3074, #1817, .T. ) ;
#3058=AXIS2_PLACEMENT_3D ( 'NONE', #6888, #1042, #9030 ) ;
#3074=VERTEX_POINT ( 'NONE', #6762 ) ;
#3078=ORIENTED_EDGE ( 'NONE', *, *, #7093, .T. ) ;
#3090=DIRECTION ( 'NONE',  ( -0.000000000000000000, 1.000000000000000000, -0.000000000000000000 ) ) ;
#3092=DIRECTION ( 'NONE',  ( -0.000000000000000000, -1.000000000000000000, -0.000000000000000000 ) ) ;
#3102=EDGE_CURVE ( 'NONE', #3626, #7297, #12332, .T. ) ;
#3147=ORIENTED_EDGE ( 'NONE', *, *, #8767, .F. ) ;
#3172=EDGE_CURVE ( 'NONE', #12462, #2380, #10052, .T. ) ;
#3198=CIRCLE ( 'NONE', #6872, 0.03999999999999998002 ) ;
#3207=EDGE_CURVE ( 'NONE', #11406, #1865, #10358, .T. ) ;
#3222=DIRECTION ( 'NONE',  ( 0.000000000000000000, 0.000000000000000000, 1.000000000000000000 ) ) ;
#3245=ADVANCED_FACE ( 'NONE', ( #5857 ), #4548, .F. ) ;
#3264=CIRCLE ( 'NONE', #12295, 0.03999999999999998002 ) ;
#3295=DIRECTION ( 'NONE',  ( 0.000000000000000000, 0.000000000000000000, -1.000000000000000000 ) ) ;
#3299=DIRECTION ( 'NONE',  ( 0.000000000000000000, -1.000000000000000000, 0.000000000000000000 ) ) ;
#3318=CARTESIAN_POINT ( 'NONE',  ( 0.8999999999999998002, 0.000000000000000000, -0.3799999999999999489 ) ) ;
#3348=ORIENTED_EDGE ( 'NONE', *, *, #12591, .T. ) ;
#3355=EDGE_CURVE ( 'NONE', #15055, #15129, #108, .T. ) ;
#3364=CARTESIAN_POINT ( 'NONE',  ( 1.564978703518703940, 0.1749999999999999889, -0.4193347797797316034 ) ) ;
#3392=ORIENTED_EDGE ( 'NONE', *, *, #6259, .F. ) ;
#3396=DIRECTION ( 'NONE',  ( 0.000000000000000000, 0.000000000000000000, -1.000000000000000000 ) ) ;
#3413=ORIENTED_EDGE ( 'NONE', *, *, #4873, .F. ) ;
#3434=PLANE ( 'NONE',  #3058 ) ;
#3454=CARTESIAN_POINT ( 'NONE',  ( 0.4125000000000000333, 0.000000000000000000, -0.3724999999999999978 ) ) ;
#3455=ORIENTED_EDGE ( 'NONE', *, *, #9576, .F. ) ;
#3456=CIRCLE ( 'NONE', #14196, 0.8000000000000000444 ) ;
#3460=DIRECTION ( 'NONE',  ( 0.000000000000000000, -1.000000000000000000, 0.000000000000000000 ) ) ;
#3501=CARTESIAN_POINT ( 'NONE',  ( 0.8999999999999998002, 0.1549999999999996103, -0.2949999999999999289 ) ) ;
#3505=( NAMED_UNIT ( * ) SI_UNIT ( $, .STERADIAN. ) SOLID_ANGLE_UNIT ( ) );
#3525=VERTEX_POINT ( 'NONE', #4054 ) ;
#3526=ORIENTED_EDGE ( 'NONE', *, *, #3999, .F. ) ;
#3539=CARTESIAN_POINT ( 'NONE',  ( 0.5400755080658357077, 0.1749999999999999889, -1.532626322880899838 ) ) ;
#3558=AXIS2_PLACEMENT_3D ( 'NONE', #8128, #2456, #3295 ) ;
#3584=ORIENTED_EDGE ( 'NONE', *, *, #12872, .T. ) ;
#3596=CARTESIAN_POINT ( 'NONE',  ( -0.4124999999999999223, 0.000000000000000000, 0.3724999999999999978 ) ) ;
#3607=FACE_BOUND ( 'NONE', #6697, .T. ) ;
#3613=VERTEX_POINT ( 'NONE', #5662 ) ;
#3616=CARTESIAN_POINT ( 'NONE',  ( -0.4124999999999999223, 0.1749999999999999889, -0.4124999999999999778 ) ) ;
#3618=AXIS2_PLACEMENT_3D ( 'NONE', #7124, #3815, #9565 ) ;
#3625=CARTESIAN_POINT ( 'NONE',  ( 0.4529333289293680509, 0.1749999999999999889, -1.690370196005881009 ) ) ;
#3626=VERTEX_POINT ( 'NONE', #10320 ) ;
#3649=DIRECTION ( 'NONE',  ( 1.000000000000000000, 0.000000000000000000, 0.000000000000000000 ) ) ;
#3657=DIRECTION ( 'NONE',  ( 0.000000000000000000, 0.000000000000000000, -1.000000000000000000 ) ) ;
#3688=FACE_OUTER_BOUND ( 'NONE', #6031, .T. ) ;
#3696=DIRECTION ( 'NONE',  ( 0.000000000000000000, -1.000000000000000000, 0.000000000000000000 ) ) ;
#3703=AXIS2_PLACEMENT_3D ( 'NONE', #3800, #6607, #8895 ) ;
#3704=CARTESIAN_POINT ( 'NONE',  ( 0.5816197779170538817, 0.1749999999999999889, -1.650520655410200099 ) ) ;
#3728=APPLICATION_CONTEXT ( 'automotive_design' ) ;
#3731=CARTESIAN_POINT ( 'NONE',  ( -0.3724999999999999423, 0.1749999999999999889, 0.4124999999999999778 ) ) ;
#3737=CARTESIAN_POINT ( 'NONE',  ( 9.797174393178826150E-17, 0.1749999999999999889, 0.8000000000000000444 ) ) ;
#3749=EDGE_CURVE ( 'NONE', #7657, #3626, #10689, .T. ) ;
#3757=DIRECTION ( 'NONE',  ( 0.000000000000000000, 1.000000000000000000, 0.000000000000000000 ) ) ;
#3759=ORIENTED_EDGE ( 'NONE', *, *, #3355, .T. ) ;
#3769=ORIENTED_EDGE ( 'NONE', *, *, #7826, .F. ) ;
#3779=VECTOR ( 'NONE', #14919, 39.37007874015748143 ) ;
#3800=CARTESIAN_POINT ( 'NONE',  ( 0.3725000000000000533, 0.1749999999999999889, -0.3724999999999999978 ) ) ;
#3815=DIRECTION ( 'NONE',  ( 0.000000000000000000, 1.000000000000000000, -0.000000000000000000 ) ) ;
#3838=ORIENTED_EDGE ( 'NONE', *, *, #5518, .T. ) ;
#3852=EDGE_LOOP ( 'NONE', ( #4682, #11442, #13630, #1805 ) ) ;
#3859=CARTESIAN_POINT ( 'NONE',  ( 0.7936328852534487721, 0.000000000000000000, -0.1007315414569158740 ) ) ;
#3860=DIRECTION ( 'NONE',  ( 0.000000000000000000, 0.000000000000000000, -1.000000000000000000 ) ) ;
#3864=CARTESIAN_POINT ( 'NONE',  ( 0.8999999999999998002, 0.1749999999999999889, -0.4850000000000006528 ) ) ;
#3892=ORIENTED_EDGE ( 'NONE', *, *, #6160, .T. ) ;
#3899=DIRECTION ( 'NONE',  ( 0.000000000000000000, 0.000000000000000000, 1.000000000000000000 ) ) ;
#3941=ORIENTED_EDGE ( 'NONE', *, *, #12214, .T. ) ;
#3950=EDGE_CURVE ( 'NONE', #2859, #1313, #7552, .T. ) ;
#3951=CIRCLE ( 'NONE', #14697, 0.1249999999999999861 ) ;
#3956=DIRECTION ( 'NONE',  ( 0.000000000000000000, 0.000000000000000000, -1.000000000000000000 ) ) ;
#3967=CARTESIAN_POINT ( 'NONE',  ( -0.3724999999999999423, 0.1749999999999999889, -0.3724999999999999978 ) ) ;
#3999=EDGE_CURVE ( 'NONE', #1865, #5661, #10079, .T. ) ;
#4000=CYLINDRICAL_SURFACE ( 'NONE', #12171, 0.1249999999999999029 ) ;
#4022=ORIENTED_EDGE ( 'NONE', *, *, #8339, .T. ) ;
#4054=CARTESIAN_POINT ( 'NONE',  ( -0.3724999999999999423, 0.1749999999999999889, -0.4124999999999999778 ) ) ;
#4071=LINE ( 'NONE', #12250, #6585 ) ;
#4108=CARTESIAN_POINT ( 'NONE',  ( -0.4124999999999999223, 0.1749999999999999889, -0.4124999999999999778 ) ) ;
#4134=VERTEX_POINT ( 'NONE', #4987 ) ;
#4135=AXIS2_PLACEMENT_3D ( 'NONE', #5074, #12734, #4416 ) ;
#4175=DIRECTION ( 'NONE',  ( 0.000000000000000000, 1.000000000000000000, -0.000000000000000000 ) ) ;
#4234=CYLINDRICAL_SURFACE ( 'NONE', #3703, 0.03999999999999998002 ) ;
#4238=CARTESIAN_POINT ( 'NONE',  ( 1.564978703518703496, 0.1749999999999999889, -0.4193347797797316034 ) ) ;
#4265=DIRECTION ( 'NONE',  ( 0.000000000000000000, 1.000000000000000000, 0.000000000000000000 ) ) ;
#4299=CARTESIAN_POINT ( 'NONE',  ( 0.4125000000000000333, 0.1749999999999999889, -0.4124999999999999778 ) ) ;
#4306=AXIS2_PLACEMENT_3D ( 'NONE', #7283, #3757, #13522 ) ;
#4337=CYLINDRICAL_SURFACE ( 'NONE', #10747, 0.08500000000000004774 ) ;
#4370=EDGE_CURVE ( 'NONE', #3613, #14462, #11466, .T. ) ;
#4391=VERTEX_POINT ( 'NONE', #11385 ) ;
#4416=DIRECTION ( 'NONE',  ( 0.000000000000000000, 0.000000000000000000, -1.000000000000000000 ) ) ;
#4425=CYLINDRICAL_SURFACE ( 'NONE', #6678, 0.03999999999999998002 ) ;
#4429=ORIENTED_EDGE ( 'NONE', *, *, #2248, .T. ) ;
#4452=VERTEX_POINT ( 'NONE', #12749 ) ;
#4456=LINE ( 'NONE', #10196, #12253 ) ;
#4480=UNCERTAINTY_MEASURE_WITH_UNIT (LENGTH_MEASURE( 1.000000000000000082E-05 ), #321, 'distance_accuracy_value', 'NONE');
#4485=DIRECTION ( 'NONE',  ( 0.000000000000000000, 0.000000000000000000, -1.000000000000000000 ) ) ;
#4512=DIRECTION ( 'NONE',  ( -0.000000000000000000, -1.000000000000000000, -0.000000000000000000 ) ) ;
#4527=FACE_OUTER_BOUND ( 'NONE', #11271, .T. ) ;
#4545=LINE ( 'NONE', #9372, #10596 ) ;
#4548=PLANE ( 'NONE',  #9181 ) ;
#4563=DIRECTION ( 'NONE',  ( 0.000000000000000000, 1.000000000000000000, -0.000000000000000000 ) ) ;
#4629=AXIS2_PLACEMENT_3D ( 'NONE', #5642, #11523, #4485 ) ;
#4633=EDGE_CURVE ( 'NONE', #7622, #7601, #5299, .T. ) ;
#4636=VERTEX_POINT ( 'NONE', #7548 ) ;
#4637=ORIENTED_EDGE ( 'NONE', *, *, #1577, .F. ) ;
#4657=LINE ( 'NONE', #3737, #10186 ) ;
#4670=DIRECTION ( 'NONE',  ( 0.000000000000000000, 0.000000000000000000, -1.000000000000000000 ) ) ;
#4678=ORIENTED_EDGE ( 'NONE', *, *, #6485, .F. ) ;
#4680=LINE ( 'NONE', #4754, #603 ) ;
#4682=ORIENTED_EDGE ( 'NONE', *, *, #13600, .F. ) ;
#4690=DIRECTION ( 'NONE',  ( 0.000000000000000000, 0.000000000000000000, 1.000000000000000000 ) ) ;
#4707=DIRECTION ( 'NONE',  ( 0.000000000000000000, 1.000000000000000000, -0.000000000000000000 ) ) ;
#4754=CARTESIAN_POINT ( 'NONE',  ( -0.4124999999999999223, 0.1749999999999999889, 0.4124999999999999778 ) ) ;
#4767=DIRECTION ( 'NONE',  ( -0.000000000000000000, -1.000000000000000000, -0.000000000000000000 ) ) ;
#4789=EDGE_LOOP ( 'NONE', ( #14988, #10115, #10106, #10764 ) ) ;
#4793=AXIS2_PLACEMENT_3D ( 'NONE', #9378, #12723, #14101 ) ;
#4809=DIRECTION ( 'NONE',  ( 0.000000000000000000, 1.000000000000000000, 0.000000000000000000 ) ) ;
#4832=DIRECTION ( 'NONE',  ( 0.000000000000000000, -1.000000000000000000, 0.000000000000000000 ) ) ;
#4857=LINE ( 'NONE', #12950, #13259 ) ;
#4873=EDGE_CURVE ( 'NONE', #4452, #8991, #15111, .T. ) ;
#4885=AXIS2_PLACEMENT_3D ( 'NONE', #10452, #14321, #6224 ) ;
#4909=EDGE_LOOP ( 'NONE', ( #374, #13194, #13647, #14171 ) ) ;
#4932=EDGE_CURVE ( 'NONE', #15129, #4391, #8394, .T. ) ;
#4937=DIRECTION ( 'NONE',  ( -0.000000000000000000, 1.000000000000000000, 0.000000000000000000 ) ) ;
#4987=CARTESIAN_POINT ( 'NONE',  ( 0.4125000000000000333, 0.000000000000000000, 0.3724999999999999978 ) ) ;
#5025=VECTOR ( 'NONE', #3090, 39.37007874015748143 ) ;
#5062=CARTESIAN_POINT ( 'NONE',  ( 0.000000000000000000, 0.000000000000000000, 0.000000000000000000 ) ) ;
#5071=DIRECTION ( 'NONE',  ( 0.000000000000000000, 0.000000000000000000, -1.000000000000000000 ) ) ;
#5074=CARTESIAN_POINT ( 'NONE',  ( -0.3724999999999999423, 0.1749999999999999889, 0.3724999999999999978 ) ) ;
#5089=ORIENTED_EDGE ( 'NONE', *, *, #5239, .F. ) ;
#5095=DIRECTION ( 'NONE',  ( 0.000000000000000000, 1.000000000000000000, 0.000000000000000000 ) ) ;
#5100=DIRECTION ( 'NONE',  ( 0.000000000000000000, 1.000000000000000000, 0.000000000000000000 ) ) ;
#5143=CARTESIAN_POINT ( 'NONE',  ( -0.4124999999999999223, 0.1749999999999999889, -0.3724999999999999978 ) ) ;
#5144=ADVANCED_FACE ( 'NONE', ( #5548 ), #1779, .T. ) ;
#5148=PLANE ( 'NONE',  #7632 ) ;
#5155=EDGE_CURVE ( 'NONE', #13458, #10542, #3951, .T. ) ;
#5239=EDGE_CURVE ( 'NONE', #6058, #2380, #4456, .T. ) ;
#5298=CARTESIAN_POINT ( 'NONE',  ( 1.650520655410188775, 0.1749999999999999889, -0.5816197779170857451 ) ) ;
#5299=CIRCLE ( 'NONE', #12129, 0.08500000000000004774 ) ;
#5355=EDGE_LOOP ( 'NONE', ( #3413, #7771, #8410, #7754 ) ) ;
#5406=ORIENTED_EDGE ( 'NONE', *, *, #7859, .F. ) ;
#5434=DIRECTION ( 'NONE',  ( 0.000000000000000000, 1.000000000000000000, -0.000000000000000000 ) ) ;
#5475=CIRCLE ( 'NONE', #10592, 0.1250000000000000278 ) ;
#5513=DIRECTION ( 'NONE',  ( 0.000000000000000000, 0.000000000000000000, -1.000000000000000000 ) ) ;
#5518=EDGE_CURVE ( 'NONE', #2976, #6934, #3198, .T. ) ;
#5536=DIRECTION ( 'NONE',  ( 0.000000000000000000, 0.000000000000000000, 1.000000000000000000 ) ) ;
#5548=FACE_OUTER_BOUND ( 'NONE', #2896, .T. ) ;
#5550=LINE ( 'NONE', #7762, #13649 ) ;
#5553=MANIFOLD_SOLID_BREP ( 'Chamfer1', #11825 ) ;
#5577=EDGE_LOOP ( 'NONE', ( #3147, #5736, #11409, #10126 ) ) ;
#5588=ADVANCED_FACE ( 'NONE', ( #6526 ), #4234, .F. ) ;
#5598=CIRCLE ( 'NONE', #14628, 0.03999999999999998002 ) ;
#5605=ORIENTED_EDGE ( 'NONE', *, *, #10635, .F. ) ;
#5642=CARTESIAN_POINT ( 'NONE',  ( 0.8999999999999998002, 0.1749999999999999889, -0.3799999999999999489 ) ) ;
#5661=VERTEX_POINT ( 'NONE', #6148 ) ;
#5662=CARTESIAN_POINT ( 'NONE',  ( 0.4125000000000000333, 0.1749999999999999889, 0.3724999999999999978 ) ) ;
#5702=CARTESIAN_POINT ( 'NONE',  ( 0.000000000000000000, 0.1749999999999999889, 0.000000000000000000 ) ) ;
#5714=EDGE_CURVE ( 'NONE', #616, #12557, #13455, .T. ) ;
#5736=ORIENTED_EDGE ( 'NONE', *, *, #8783, .T. ) ;
#5739=DIRECTION ( 'NONE',  ( 0.000000000000000000, -1.000000000000000000, 0.000000000000000000 ) ) ;
#5754=AXIS2_PLACEMENT_3D ( 'NONE', #12774, #3696, #2387 ) ;
#5804=VECTOR ( 'NONE', #11044, 39.37007874015748143 ) ;
#5805=VERTEX_POINT ( 'NONE', #3731 ) ;
#5836=CONICAL_SURFACE ( 'NONE', #12174, 0.08500000000000004774, 0.7853981633974541632 ) ;
#5842=VECTOR ( 'NONE', #6824, 39.37007874015748143 ) ;
#5843=LINE ( 'NONE', #2150, #6324 ) ;
#5857=FACE_OUTER_BOUND ( 'NONE', #12567, .T. ) ;
#5888=EDGE_CURVE ( 'NONE', #14656, #10542, #3456, .T. ) ;
#5908=ORIENTED_EDGE ( 'NONE', *, *, #7113, .F. ) ;
#5919=VECTOR ( 'NONE', #3649, 39.37007874015748143 ) ;
#5920=DIRECTION ( 'NONE',  ( 0.000000000000000000, 0.000000000000000000, -1.000000000000000000 ) ) ;
#6005=FACE_OUTER_BOUND ( 'NONE', #11987, .T. ) ;
#6031=EDGE_LOOP ( 'NONE', ( #12042, #4429, #146, #8324, #9900, #10693, #13893, #14922, #7587, #5406, #7873 ) ) ;
#6044=ADVANCED_FACE ( 'NONE', ( #2044 ), #10323, .T. ) ;
#6050=EDGE_LOOP ( 'NONE', ( #12517, #14003, #7015, #6285 ) ) ;
#6058=VERTEX_POINT ( 'NONE', #13905 ) ;
#6061=FACE_BOUND ( 'NONE', #13069, .T. ) ;
#6063=CARTESIAN_POINT ( 'NONE',  ( 9.797174393178826150E-17, 0.1749999999999999889, 0.8000000000000000444 ) ) ;
#6094=EDGE_CURVE ( 'NONE', #3613, #4636, #3264, .T. ) ;
#6111=ORIENTED_EDGE ( 'NONE', *, *, #2010, .F. ) ;
#6125=DIRECTION ( 'NONE',  ( -0.000000000000000000, -1.000000000000000000, -0.000000000000000000 ) ) ;
#6133=CARTESIAN_POINT ( 'NONE',  ( 0.000000000000000000, 0.000000000000000000, 0.000000000000000000 ) ) ;
#6142=LINE ( 'NONE', #5143, #8530 ) ;
#6148=CARTESIAN_POINT ( 'NONE',  ( 0.2372115730956756152, 0.1749999999999999889, -0.8852856429364902580 ) ) ;
#6153=EDGE_CURVE ( 'NONE', #4391, #14462, #9381, .T. ) ;
#6160=EDGE_CURVE ( 'NONE', #11668, #4452, #14250, .T. ) ;
#6191=CARTESIAN_POINT ( 'NONE',  ( 0.1164708448095412852, 0.1749999999999999889, -0.9176380235743023528 ) ) ;
#6197=EDGE_CURVE ( 'NONE', #5661, #1040, #5475, .T. ) ;
#6224=DIRECTION ( 'NONE',  ( 0.000000000000000000, 0.000000000000000000, -1.000000000000000000 ) ) ;
#6259=EDGE_CURVE ( 'NONE', #9681, #6058, #2540, .T. ) ;
#6285=ORIENTED_EDGE ( 'NONE', *, *, #10442, .F. ) ;
#6322=PRODUCT_DEFINITION ( 'UNKNOWN', '', #11587, #12275 ) ;
#6324=VECTOR ( 'NONE', #3460, 39.37007874015748143 ) ;
#6381=CARTESIAN_POINT ( 'NONE',  ( -0.3724999999999999423, 0.000000000000000000, -0.4124999999999999778 ) ) ;
#6408=DIRECTION ( 'NONE',  ( 0.000000000000000000, 0.000000000000000000, 1.000000000000000000 ) ) ;
#6410=CARTESIAN_POINT ( 'NONE',  ( 0.8999999999999998002, 0.000000000000000000, -0.2749999999999998557 ) ) ;
#6424=ORIENTED_EDGE ( 'NONE', *, *, #4873, .T. ) ;
#6485=EDGE_CURVE ( 'NONE', #12151, #7622, #13606, .T. ) ;
#6526=FACE_OUTER_BOUND ( 'NONE', #11284, .T. ) ;
#6535=CARTESIAN_POINT ( 'NONE',  ( 0.1007315414569005807, 0.1749999999999999889, -0.7936328852534507705 ) ) ;
#6548=VERTEX_POINT ( 'NONE', #57 ) ;
#6583=FACE_OUTER_BOUND ( 'NONE', #13043, .T. ) ;
#6585=VECTOR ( 'NONE', #9047, 39.37007874015748143 ) ;
#6596=CIRCLE ( 'NONE', #12697, 0.1050000000000001071 ) ;
#6607=DIRECTION ( 'NONE',  ( 0.000000000000000000, 1.000000000000000000, -0.000000000000000000 ) ) ;
#6616=EDGE_CURVE ( 'NONE', #2859, #3525, #7202, .T. ) ;
#6662=ORIENTED_EDGE ( 'NONE', *, *, #260, .T. ) ;
#6664=DIRECTION ( 'NONE',  ( -0.2588190451024959260, 0.000000000000000000, 0.9659258262890748625 ) ) ;
#6678=AXIS2_PLACEMENT_3D ( 'NONE', #12589, #4809, #12900 ) ;
#6697=EDGE_LOOP ( 'NONE', ( #8499, #2624 ) ) ;
#6715=AXIS2_PLACEMENT_3D ( 'NONE', #2689, #12639, #8368 ) ;
#6755=DIRECTION ( 'NONE',  ( 0.000000000000000000, 0.000000000000000000, -1.000000000000000000 ) ) ;
#6762=CARTESIAN_POINT ( 'NONE',  ( 0.000000000000000000, 0.1749999999999999889, -0.8000000000000000444 ) ) ;
#6824=DIRECTION ( 'NONE',  ( -1.000000000000000000, -0.000000000000000000, -0.000000000000000000 ) ) ;
#6860=DIRECTION ( 'NONE',  ( -0.000000000000000000, -1.000000000000000000, -0.000000000000000000 ) ) ;
#6872=AXIS2_PLACEMENT_3D ( 'NONE', #8399, #13037, #3657 ) ;
#6888=CARTESIAN_POINT ( 'NONE',  ( -0.4124999999999999223, 0.1749999999999999889, -0.4124999999999999778 ) ) ;
#6895=ADVANCED_FACE ( 'NONE', ( #7938 ), #4425, .F. ) ;
#6926=DIRECTION ( 'NONE',  ( -0.9659258262890698665, 0.000000000000000000, 0.2588190451025147443 ) ) ;
#6933=EDGE_LOOP ( 'NONE', ( #1478, #3526, #1424, #5908 ) ) ;
#6934=VERTEX_POINT ( 'NONE', #7117 ) ;
#6947=AXIS2_PLACEMENT_3D ( 'NONE', #2288, #9781, #8633 ) ;
#6981=CARTESIAN_POINT ( 'NONE',  ( 0.3725000000000000533, 0.000000000000000000, -0.4124999999999999778 ) ) ;
#6983=CARTESIAN_POINT ( 'NONE',  ( 0.8999999999999998002, 0.000000000000000000, -0.3799999999999999489 ) ) ;
#6988=FACE_OUTER_BOUND ( 'NONE', #140, .T. ) ;
#6999=ORIENTED_EDGE ( 'NONE', *, *, #532, .F. ) ;
#7015=ORIENTED_EDGE ( 'NONE', *, *, #8358, .T. ) ;
#7059=ORIENTED_EDGE ( 'NONE', *, *, #14930, .F. ) ;
#7093=EDGE_CURVE ( 'NONE', #14462, #15055, #7334, .T. ) ;
#7100=UNCERTAINTY_MEASURE_WITH_UNIT (LENGTH_MEASURE( 1.000000000000000082E-05 ), #2204, 'distance_accuracy_value', 'NONE');
#7113=EDGE_CURVE ( 'NONE', #1040, #6548, #13400, .T. ) ;
#7117=CARTESIAN_POINT ( 'NONE',  ( -0.4124999999999999223, 0.000000000000000000, -0.3724999999999999978 ) ) ;
#7124=CARTESIAN_POINT ( 'NONE',  ( 0.000000000000000000, 0.000000000000000000, 0.000000000000000000 ) ) ;
#7127=FACE_OUTER_BOUND ( 'NONE', #11821, .T. ) ;
#7130=STYLED_ITEM('',(#15206),#5553);
#7133=CARTESIAN_POINT ( 'NONE',  ( 0.1007315414569005807, 0.1749999999999999889, -0.7936328852534507705 ) ) ;
#7149=CARTESIAN_POINT ( 'NONE',  ( 0.8852856429364857060, 0.000000000000000000, -0.2372115730956926294 ) ) ;
#7171=LINE ( 'NONE', #8090, #2628 ) ;
#7172=CARTESIAN_POINT ( 'NONE',  ( -0.4124999999999999223, 0.000000000000000000, 0.4124999999999999778 ) ) ;
#7202=CIRCLE ( 'NONE', #9873, 0.03999999999999998002 ) ;
#7266=CARTESIAN_POINT ( 'NONE',  ( 0.8999999999999998002, 0.1749999999999999889, -0.3799999999999999489 ) ) ;
#7270=CYLINDRICAL_SURFACE ( 'NONE', #1215, 0.1249999999999999861 ) ;
#7283=CARTESIAN_POINT ( 'NONE',  ( 0.000000000000000000, 0.000000000000000000, 0.000000000000000000 ) ) ;
#7297=VERTEX_POINT ( 'NONE', #3704 ) ;
#7300=LINE ( 'NONE', #227, #11709 ) ;
#7312=CIRCLE ( 'NONE', #4135, 0.03999999999999998002 ) ;
#7317=CIRCLE ( 'NONE', #14626, 0.1249999999999999029 ) ;
#7322=CARTESIAN_POINT ( 'NONE',  ( -0.4124999999999999223, 0.1749999999999999889, 0.4124999999999999778 ) ) ;
#7333=ORIENTED_EDGE ( 'NONE', *, *, #3102, .T. ) ;
#7334=LINE ( 'NONE', #8405, #2765 ) ;
#7358=DIRECTION ( 'NONE',  ( 0.000000000000000000, 0.000000000000000000, 1.000000000000000000 ) ) ;
#7370=CYLINDRICAL_SURFACE ( 'NONE', #13482, 0.08500000000000004774 ) ;
#7392=CARTESIAN_POINT ( 'NONE',  ( 0.8999999999999998002, 0.000000000000000000, -0.4850000000000000977 ) ) ;
#7398=AXIS2_PLACEMENT_3D ( 'NONE', #3539, #4767, #5920 ) ;
#7403=ORIENTED_EDGE ( 'NONE', *, *, #8358, .F. ) ;
#7425=EDGE_CURVE ( 'NONE', #4452, #5805, #8524, .T. ) ;
#7457=ADVANCED_FACE ( 'NONE', ( #79 ), #14091, .F. ) ;
#7469=ORIENTED_EDGE ( 'NONE', *, *, #12294, .T. ) ;
#7483=DIRECTION ( 'NONE',  ( 0.000000000000000000, 0.000000000000000000, -1.000000000000000000 ) ) ;
#7504=DIRECTION ( 'NONE',  ( 0.000000000000000000, 0.000000000000000000, -1.000000000000000000 ) ) ;
#7548=CARTESIAN_POINT ( 'NONE',  ( 0.3725000000000000533, 0.1749999999999999889, 0.4124999999999999778 ) ) ;
#7552=LINE ( 'NONE', #4108, #9227 ) ;
#7587=ORIENTED_EDGE ( 'NONE', *, *, #2250, .F. ) ;
#7601=VERTEX_POINT ( 'NONE', #8886 ) ;
#7622=VERTEX_POINT ( 'NONE', #11404 ) ;
#7632=AXIS2_PLACEMENT_3D ( 'NONE', #14459, #13374, #8655 ) ;
#7647=ADVANCED_FACE ( 'NONE', ( #12699 ), #1060, .T. ) ;
#7649=DIRECTION ( 'NONE',  ( 0.000000000000000000, 1.000000000000000000, 0.000000000000000000 ) ) ;
#7657=VERTEX_POINT ( 'NONE', #751 ) ;
#7667=LINE ( 'NONE', #8534, #2879 ) ;
#7696=VECTOR ( 'NONE', #12237, 39.37007874015748143 ) ;
#7713=ORIENTED_EDGE ( 'NONE', *, *, #2012, .F. ) ;
#7728=DIRECTION ( 'NONE',  ( 0.000000000000000000, 1.000000000000000000, 0.000000000000000000 ) ) ;
#7754=ORIENTED_EDGE ( 'NONE', *, *, #2021, .T. ) ;
#7762=CARTESIAN_POINT ( 'NONE',  ( 0.8999999999999998002, 0.000000000000000000, -0.2749999999999998557 ) ) ;
#7766=ORIENTED_EDGE ( 'NONE', *, *, #4370, .T. ) ;
#7767=DIRECTION ( 'NONE',  ( 0.000000000000000000, 0.000000000000000000, 1.000000000000000000 ) ) ;
#7771=ORIENTED_EDGE ( 'NONE', *, *, #7425, .T. ) ;
#7777=FACE_OUTER_BOUND ( 'NONE', #14790, .T. ) ;
#7784=CARTESIAN_POINT ( 'NONE',  ( -0.4124999999999999223, 0.000000000000000000, -0.4124999999999999778 ) ) ;
#7798=CONICAL_SURFACE ( 'NONE', #1429, 0.08500000000000004774, 0.7853981633974541632 ) ;
#7800=CARTESIAN_POINT ( 'NONE',  ( 0.4125000000000000333, 0.1749999999999999889, -0.4124999999999999778 ) ) ;
#7810=CONICAL_SURFACE ( 'NONE', #1203, 0.1050000000000001071, 0.7853981633974560506 ) ;
#7811=CARTESIAN_POINT ( 'NONE',  ( 0.4529333289293680509, 0.1749999999999999889, -1.690370196005881009 ) ) ;
#7826=EDGE_CURVE ( 'NONE', #5805, #4636, #4680, .T. ) ;
#7829=CARTESIAN_POINT ( 'NONE',  ( 0.8999999999999998002, 0.000000000000000000, -0.4850000000000000977 ) ) ;
#7837=DIRECTION ( 'NONE',  ( 0.000000000000000000, 0.000000000000000000, -1.000000000000000000 ) ) ;
#7843=ADVANCED_FACE ( 'NONE', ( #3607, #11861, #3688 ), #61, .T. ) ;
#7859=EDGE_CURVE ( 'NONE', #6548, #10691, #10899, .T. ) ;
#7873=ORIENTED_EDGE ( 'NONE', *, *, #2865, .T. ) ;
#7878=CARTESIAN_POINT ( 'NONE',  ( 0.5400755080658357077, 0.000000000000000000, -1.532626322880899838 ) ) ;
#7896=CARTESIAN_POINT ( 'NONE',  ( 0.2372115730956756152, 0.000000000000000000, -0.8852856429364902580 ) ) ;
#7930=ORIENTED_EDGE ( 'NONE', *, *, #13561, .F. ) ;
#7938=FACE_OUTER_BOUND ( 'NONE', #4909, .T. ) ;
#7955=CIRCLE ( 'NONE', #3558, 0.1249999999999999029 ) ;
#7973=DIRECTION ( 'NONE',  ( -0.000000000000000000, -1.000000000000000000, -0.000000000000000000 ) ) ;
#8034=ORIENTED_EDGE ( 'NONE', *, *, #3749, .T. ) ;
#8047=CIRCLE ( 'NONE', #1919, 0.08500000000000004774 ) ;
#8060=AXIS2_PLACEMENT_3D ( 'NONE', #14667, #2814, #7483 ) ;
#8080=VECTOR ( 'NONE', #5739, 39.37007874015748143 ) ;
#8090=CARTESIAN_POINT ( 'NONE',  ( 0.8999999999999998002, 0.1749999999999999889, -0.2949999999999999289 ) ) ;
#8125=VERTEX_POINT ( 'NONE', #13587 ) ;
#8128=CARTESIAN_POINT ( 'NONE',  ( 0.5400755080658357077, 0.000000000000000000, -1.532626322880899838 ) ) ;
#8144=CARTESIAN_POINT ( 'NONE',  ( 0.4193347797797013499, 0.1749999999999999889, -1.564978703518711711 ) ) ;
#8183=DIRECTION ( 'NONE',  ( 0.000000000000000000, 0.7071067811865432429, 0.7071067811865516806 ) ) ;
#8284=ORIENTED_EDGE ( 'NONE', *, *, #8767, .T. ) ;
#8298=DIRECTION ( 'NONE',  ( -1.000000000000000000, -0.000000000000000000, -0.000000000000000000 ) ) ;
#8301=LINE ( 'NONE', #7149, #1664 ) ;
#8311=DIRECTION ( 'NONE',  ( 0.9659258262890749736, -0.000000000000000000, 0.2588190451024959815 ) ) ;
#8316=CARTESIAN_POINT ( 'NONE',  ( 0.4529333289293680509, 0.000000000000000000, -1.690370196005881009 ) ) ;
#8324=ORIENTED_EDGE ( 'NONE', *, *, #3749, .F. ) ;
#8339=EDGE_CURVE ( 'NONE', #2140, #14656, #4657, .T. ) ;
#8354=DIRECTION ( 'NONE',  ( 0.000000000000000000, 0.000000000000000000, -1.000000000000000000 ) ) ;
#8358=EDGE_CURVE ( 'NONE', #12649, #8125, #2586, .T. ) ;
#8368=DIRECTION ( 'NONE',  ( 0.000000000000000000, 0.000000000000000000, -1.000000000000000000 ) ) ;
#8388=ADVANCED_BREP_SHAPE_REPRESENTATION ( '', ( #5553, #8424 ), #3023 ) ;
#8394=LINE ( 'NONE', #12963, #10555 ) ;
#8399=CARTESIAN_POINT ( 'NONE',  ( -0.3724999999999999423, 0.000000000000000000, -0.3724999999999999978 ) ) ;
#8405=CARTESIAN_POINT ( 'NONE',  ( 0.4125000000000000333, 0.000000000000000000, -0.3724999999999999978 ) ) ;
#8410=ORIENTED_EDGE ( 'NONE', *, *, #7826, .T. ) ;
#8419=DIRECTION ( 'NONE',  ( 0.000000000000000000, 1.000000000000000000, -0.000000000000000000 ) ) ;
#8424=AXIS2_PLACEMENT_3D ( 'NONE', #5062, #7358, #1521 ) ;
#8452=ORIENTED_EDGE ( 'NONE', *, *, #8339, .F. ) ;
#8465=AXIS2_PLACEMENT_3D ( 'NONE', #6133, #4832, #11637 ) ;
#8485=SHAPE_DEFINITION_REPRESENTATION ( #770, #8950 ) ;
#8499=ORIENTED_EDGE ( 'NONE', *, *, #5714, .T. ) ;
#8522=EDGE_CURVE ( 'NONE', #3074, #10691, #11360, .T. ) ;
#8524=LINE ( 'NONE', #13166, #13309 ) ;
#8530=VECTOR ( 'NONE', #13080, 39.37007874015748143 ) ;
#8531=DIRECTION ( 'NONE',  ( 0.000000000000000000, 1.000000000000000000, -0.000000000000000000 ) ) ;
#8534=CARTESIAN_POINT ( 'NONE',  ( 0.8999999999999998002, 0.1549999999999996103, -0.4650000000000000244 ) ) ;
#8554=CIRCLE ( 'NONE', #2686, 0.1250000000000000278 ) ;
#8589=DIRECTION ( 'NONE',  ( 0.000000000000000000, 0.000000000000000000, -1.000000000000000000 ) ) ;
#8633=DIRECTION ( 'NONE',  ( 0.000000000000000000, 0.000000000000000000, -1.000000000000000000 ) ) ;
#8655=DIRECTION ( 'NONE',  ( 1.000000000000000000, 0.000000000000000000, -0.000000000000000000 ) ) ;
#8657=DIRECTION ( 'NONE',  ( 0.2588190451024959260, 0.000000000000000000, -0.9659258262890748625 ) ) ;
#8695=DIRECTION ( 'NONE',  ( -0.000000000000000000, -1.000000000000000000, -0.000000000000000000 ) ) ;
#8723=DIMENSIONAL_EXPONENTS ( 1.000000000000000000, 0.000000000000000000, 0.000000000000000000, 0.000000000000000000, 0.000000000000000000, 0.000000000000000000, 0.000000000000000000 ) ;
#8724=VECTOR ( 'NONE', #784, 39.37007874015748143 ) ;
#8733=EDGE_CURVE ( 'NONE', #7297, #10755, #14329, .T. ) ;
#8736=ORIENTED_EDGE ( 'NONE', *, *, #3950, .F. ) ;
#8767=EDGE_CURVE ( 'NONE', #12649, #7601, #7171, .T. ) ;
#8783=EDGE_CURVE ( 'NONE', #12649, #12151, #12383, .T. ) ;
#8797=EDGE_CURVE ( 'NONE', #7622, #616, #10978, .T. ) ;
#8885=DIRECTION ( 'NONE',  ( 0.000000000000000000, 1.000000000000000000, -0.000000000000000000 ) ) ;
#8886=CARTESIAN_POINT ( 'NONE',  ( 0.8999999999999998002, 0.01999999999999975409, -0.2949999999999999289 ) ) ;
#8895=DIRECTION ( 'NONE',  ( 0.000000000000000000, 0.000000000000000000, 1.000000000000000000 ) ) ;
#8899=DIRECTION ( 'NONE',  ( 0.000000000000000000, 1.000000000000000000, 0.000000000000000000 ) ) ;
#8950=SHAPE_REPRESENTATION ( 'Lock Lever', ( #8424 ), #3023 ) ;
#8991=VERTEX_POINT ( 'NONE', #702 ) ;
#8999=ORIENTED_EDGE ( 'NONE', *, *, #13788, .T. ) ;
#9030=DIRECTION ( 'NONE',  ( 0.000000000000000000, 0.000000000000000000, -1.000000000000000000 ) ) ;
#9047=DIRECTION ( 'NONE',  ( -0.000000000000000000, -0.000000000000000000, -1.000000000000000000 ) ) ;
#9138=AXIS2_PLACEMENT_3D ( 'NONE', #13746, #4512, #4670 ) ;
#9148=ADVANCED_FACE ( 'NONE', ( #9217 ), #1294, .F. ) ;
#9181=AXIS2_PLACEMENT_3D ( 'NONE', #11660, #9374, #6926 ) ;
#9217=FACE_OUTER_BOUND ( 'NONE', #6933, .T. ) ;
#9227=VECTOR ( 'NONE', #6408, 39.37007874015748143 ) ;
#9265=CIRCLE ( 'NONE', #4629, 0.1050000000000006622 ) ;
#9278=ORIENTED_EDGE ( 'NONE', *, *, #8522, .T. ) ;
#9288=CARTESIAN_POINT ( 'NONE',  ( 0.8852856429364857060, 0.000000000000000000, -0.2372115730956926571 ) ) ;
#9359=DIRECTION ( 'NONE',  ( -0.000000000000000000, -1.000000000000000000, -0.000000000000000000 ) ) ;
#9372=CARTESIAN_POINT ( 'NONE',  ( 0.7727406610312560487, 0.000000000000000000, -0.2070552360820117899 ) ) ;
#9374=DIRECTION ( 'NONE',  ( -0.2588190451025147443, 0.000000000000000000, -0.9659258262890698665 ) ) ;
#9378=CARTESIAN_POINT ( 'NONE',  ( 0.8999999999999998002, 0.000000000000000000, -0.3799999999999999489 ) ) ;
#9381=CIRCLE ( 'NONE', #11818, 0.03999999999999998002 ) ;
#9409=SHAPE_REPRESENTATION_RELATIONSHIP ( 'NONE' , 'NONE' ,  #8950, #8388 ) ;
#9503=ORIENTED_EDGE ( 'NONE', *, *, #3999, .T. ) ;
#9528=ADVANCED_FACE ( 'NONE', ( #6583 ), #3434, .T. ) ;
#9537=CARTESIAN_POINT ( 'NONE',  ( 0.1164708448095412852, 0.000000000000000000, -0.9176380235743023528 ) ) ;
#9565=DIRECTION ( 'NONE',  ( 0.000000000000000000, 0.000000000000000000, -1.000000000000000000 ) ) ;
#9576=EDGE_CURVE ( 'NONE', #8125, #2908, #1336, .T. ) ;
#9592=CARTESIAN_POINT ( 'NONE',  ( 0.3725000000000000533, 0.000000000000000000, 0.3724999999999999978 ) ) ;
#9596=EDGE_LOOP ( 'NONE', ( #1399, #12496, #13930, #7059 ) ) ;
#9604=DIRECTION ( 'NONE',  ( -0.000000000000000000, -1.000000000000000000, -0.000000000000000000 ) ) ;
#9622=VECTOR ( 'NONE', #3092, 39.37007874015748143 ) ;
#9671=ORIENTED_EDGE ( 'NONE', *, *, #2250, .T. ) ;
#9675=AXIS2_PLACEMENT_3D ( 'NONE', #3625, #8311, #8657 ) ;
#9681=VERTEX_POINT ( 'NONE', #2881 ) ;
#9691=LENGTH_MEASURE_WITH_UNIT ( LENGTH_MEASURE( 0.02539999999999999897 ), #10048 );
#9718=ORIENTED_EDGE ( 'NONE', *, *, #9576, .T. ) ;
#9750=VECTOR ( 'NONE', #12217, 39.37007874015748143 ) ;
#9780=CYLINDRICAL_SURFACE ( 'NONE', #10658, 0.03999999999999998002 ) ;
#9781=DIRECTION ( 'NONE',  ( -0.000000000000000000, -1.000000000000000000, 0.000000000000000000 ) ) ;
#9787=ORIENTED_EDGE ( 'NONE', *, *, #7093, .F. ) ;
#9827=DIRECTION ( 'NONE',  ( 0.000000000000000000, 0.000000000000000000, 1.000000000000000000 ) ) ;
#9828=PRODUCT ( 'Lock Lever', 'Lock Lever', '', ( #12139 ) ) ;
#9839=AXIS2_PLACEMENT_3D ( 'NONE', #13315, #534, #1994 ) ;
#9844=ORIENTED_EDGE ( 'NONE', *, *, #8797, .T. ) ;
#9861=EDGE_LOOP ( 'NONE', ( #14560, #9503, #965, #6662 ) ) ;
#9873=AXIS2_PLACEMENT_3D ( 'NONE', #3967, #2895, #1658 ) ;
#9875=ORIENTED_EDGE ( 'NONE', *, *, #1577, .T. ) ;
#9900=ORIENTED_EDGE ( 'NONE', *, *, #12708, .T. ) ;
#10001=ORIENTED_EDGE ( 'NONE', *, *, #12294, .F. ) ;
#10003=AXIS2_PLACEMENT_3D ( 'NONE', #13331, #5100, #14649 ) ;
#10016=CYLINDRICAL_SURFACE ( 'NONE', #11879, 0.8000000000000000444 ) ;
#10033=CARTESIAN_POINT ( 'NONE',  ( 0.8999999999999998002, 0.1549999999999996103, -0.3799999999999999489 ) ) ;
#10045=ORIENTED_EDGE ( 'NONE', *, *, #12708, .F. ) ;
#10048=( LENGTH_UNIT ( ) NAMED_UNIT ( * ) SI_UNIT ( $, .METRE. ) );
#10052=LINE ( 'NONE', #4238, #5025 ) ;
#10070=ORIENTED_EDGE ( 'NONE', *, *, #11892, .T. ) ;
#10079=LINE ( 'NONE', #14734, #11182 ) ;
#10087=FACE_OUTER_BOUND ( 'NONE', #4789, .T. ) ;
#10093=ORIENTED_EDGE ( 'NONE', *, *, #10391, .F. ) ;
#10097=ADVANCED_FACE ( 'NONE', ( #472 ), #5836, .F. ) ;
#10106=ORIENTED_EDGE ( 'NONE', *, *, #7113, .T. ) ;
#10111=EDGE_CURVE ( 'NONE', #10542, #9681, #7300, .T. ) ;
#10115=ORIENTED_EDGE ( 'NONE', *, *, #3047, .F. ) ;
#10121=DIRECTION ( 'NONE',  ( 0.000000000000000000, 1.000000000000000000, -0.000000000000000000 ) ) ;
#10126=ORIENTED_EDGE ( 'NONE', *, *, #4633, .T. ) ;
#10148=CARTESIAN_POINT ( 'NONE',  ( 0.000000000000000000, 0.1749999999999999889, -0.8000000000000000444 ) ) ;
#10186=VECTOR ( 'NONE', #10618, 39.37007874015748143 ) ;
#10196=CARTESIAN_POINT ( 'NONE',  ( 0.7727406610312560487, 0.1749999999999999889, -0.2070552360820117899 ) ) ;
#10245=VERTEX_POINT ( 'NONE', #8144 ) ;
#10248=ORIENTED_EDGE ( 'NONE', *, *, #10635, .T. ) ;
#10253=CARTESIAN_POINT ( 'NONE',  ( 0.3725000000000000533, 0.1749999999999999889, 0.3724999999999999978 ) ) ;
#10278=CARTESIAN_POINT ( 'NONE',  ( 0.000000000000000000, 0.1749999999999999889, 0.000000000000000000 ) ) ;
#10291=( GEOMETRIC_REPRESENTATION_CONTEXT ( 3 ) GLOBAL_UNCERTAINTY_ASSIGNED_CONTEXT ( ( #4480 ) ) GLOBAL_UNIT_ASSIGNED_CONTEXT ( ( #321, #11983, #12326 ) ) REPRESENTATION_CONTEXT ( 'NONE', 'WORKASPACE' ) );
#10313=ORIENTED_EDGE ( 'NONE', *, *, #13239, .T. ) ;
#10315=ORIENTED_EDGE ( 'NONE', *, *, #1257, .T. ) ;
#10320=CARTESIAN_POINT ( 'NONE',  ( 0.5816197779170538817, 0.000000000000000000, -1.650520655410200099 ) ) ;
#10323=CYLINDRICAL_SURFACE ( 'NONE', #9138, 0.1250000000000000278 ) ;
#10328=FACE_OUTER_BOUND ( 'NONE', #12674, .T. ) ;
#10358=LINE ( 'NONE', #8316, #2573 ) ;
#10391=EDGE_CURVE ( 'NONE', #5805, #1313, #7312, .T. ) ;
#10394=ORIENTED_EDGE ( 'NONE', *, *, #3047, .T. ) ;
#10404=DIRECTION ( 'NONE',  ( -0.000000000000000000, -1.000000000000000000, 0.000000000000000000 ) ) ;
#10424=CARTESIAN_POINT ( 'NONE',  ( 0.000000000000000000, 0.1749999999999999889, 0.000000000000000000 ) ) ;
#10433=DIRECTION ( 'NONE',  ( 0.9659258262890698665, 0.000000000000000000, -0.2588190451025147443 ) ) ;
#10442=EDGE_CURVE ( 'NONE', #2908, #8125, #9265, .T. ) ;
#10449=ORIENTED_EDGE ( 'NONE', *, *, #14764, .T. ) ;
#10452=CARTESIAN_POINT ( 'NONE',  ( 0.000000000000000000, 0.1749999999999999889, 0.000000000000000000 ) ) ;
#10455=ORIENTED_EDGE ( 'NONE', *, *, #6197, .T. ) ;
#10462=ORIENTED_EDGE ( 'NONE', *, *, #11715, .T. ) ;
#10464=EDGE_LOOP ( 'NONE', ( #8034, #7333, #14007, #781 ) ) ;
#10533=ADVANCED_FACE ( 'NONE', ( #7777 ), #4337, .F. ) ;
#10537=ADVANCED_FACE ( 'NONE', ( #1102 ), #2423, .T. ) ;
#10542=VERTEX_POINT ( 'NONE', #3859 ) ;
#10549=ORIENTED_EDGE ( 'NONE', *, *, #14930, .T. ) ;
#10555=VECTOR ( 'NONE', #11752, 39.37007874015748143 ) ;
#10565=ORIENTED_EDGE ( 'NONE', *, *, #2125, .T. ) ;
#10586=ORIENTED_EDGE ( 'NONE', *, *, #2307, .T. ) ;
#10592=AXIS2_PLACEMENT_3D ( 'NONE', #6191, #2743, #6755 ) ;
#10596=VECTOR ( 'NONE', #10433, 39.37007874015748854 ) ;
#10618=DIRECTION ( 'NONE',  ( -0.000000000000000000, -1.000000000000000000, -0.000000000000000000 ) ) ;
#10635=EDGE_CURVE ( 'NONE', #4134, #15055, #4071, .T. ) ;
#10639=DIRECTION ( 'NONE',  ( 1.000000000000000000, 0.000000000000000000, 0.000000000000000000 ) ) ;
#10658=AXIS2_PLACEMENT_3D ( 'NONE', #10930, #12990, #3899 ) ;
#10670=CYLINDRICAL_SURFACE ( 'NONE', #409, 0.03999999999999998002 ) ;
#10689=CIRCLE ( 'NONE', #3618, 1.749999999999999556 ) ;
#10691=VERTEX_POINT ( 'NONE', #11410 ) ;
#10693=ORIENTED_EDGE ( 'NONE', *, *, #14764, .F. ) ;
#10732=CYLINDRICAL_SURFACE ( 'NONE', #930, 1.749999999999999556 ) ;
#10747=AXIS2_PLACEMENT_3D ( 'NONE', #13654, #15113, #11677 ) ;
#10755=VERTEX_POINT ( 'NONE', #3045 ) ;
#10764=ORIENTED_EDGE ( 'NONE', *, *, #7859, .T. ) ;
#10774=ADVANCED_FACE ( 'NONE', ( #4527 ), #7810, .F. ) ;
#10820=ORIENTED_EDGE ( 'NONE', *, *, #6616, .T. ) ;
#10835=ORIENTED_EDGE ( 'NONE', *, *, #3172, .F. ) ;
#10887=ORIENTED_EDGE ( 'NONE', *, *, #532, .T. ) ;
#10899=CIRCLE ( 'NONE', #4306, 0.8000000000000000444 ) ;
#10925=EDGE_LOOP ( 'NONE', ( #6999, #4022, #2950, #767 ) ) ;
#10930=CARTESIAN_POINT ( 'NONE',  ( -0.3724999999999999423, 0.1749999999999999889, -0.3724999999999999978 ) ) ;
#10952=CARTESIAN_POINT ( 'NONE',  ( 0.8999999999999998002, 0.1749999999999999889, -0.3799999999999999489 ) ) ;
#10953=VECTOR ( 'NONE', #6664, 39.37007874015748854 ) ;
#10978=LINE ( 'NONE', #7392, #5804 ) ;
#11044=DIRECTION ( 'NONE',  ( 0.000000000000000000, -0.7071067811865421326, -0.7071067811865530128 ) ) ;
#11054=ORIENTED_EDGE ( 'NONE', *, *, #13600, .T. ) ;
#11075=ORIENTED_EDGE ( 'NONE', *, *, #2248, .F. ) ;
#11102=LINE ( 'NONE', #1987, #2779 ) ;
#11166=DIRECTION ( 'NONE',  ( 0.000000000000000000, 0.000000000000000000, 1.000000000000000000 ) ) ;
#11168=LINE ( 'NONE', #7811, #10953 ) ;
#11171=ORIENTED_EDGE ( 'NONE', *, *, #4370, .F. ) ;
#11182=VECTOR ( 'NONE', #4265, 39.37007874015748143 ) ;
#11247=DIRECTION ( 'NONE',  ( -0.000000000000000000, -1.000000000000000000, -0.000000000000000000 ) ) ;
#11254=CARTESIAN_POINT ( 'NONE',  ( 0.000000000000000000, 0.1749999999999999889, 0.000000000000000000 ) ) ;
#11271=EDGE_LOOP ( 'NONE', ( #14159, #10070, #1264, #14042 ) ) ;
#11284=EDGE_LOOP ( 'NONE', ( #2570, #689, #14950, #9787 ) ) ;
#11301=CIRCLE ( 'NONE', #9839, 0.8000000000000000444 ) ;
#11360=LINE ( 'NONE', #10148, #8724 ) ;
#11374=CONICAL_SURFACE ( 'NONE', #4793, 0.1050000000000001071, 0.7853981633974560506 ) ;
#11385=CARTESIAN_POINT ( 'NONE',  ( 0.3725000000000000533, 0.1749999999999999889, -0.4124999999999999778 ) ) ;
#11404=CARTESIAN_POINT ( 'NONE',  ( 0.8999999999999998002, 0.01999999999999975409, -0.4650000000000000244 ) ) ;
#11406=VERTEX_POINT ( 'NONE', #13575 ) ;
#11409=ORIENTED_EDGE ( 'NONE', *, *, #6485, .T. ) ;
#11410=CARTESIAN_POINT ( 'NONE',  ( 0.000000000000000000, 0.000000000000000000, -0.8000000000000000444 ) ) ;
#11420=DIRECTION ( 'NONE',  ( 0.000000000000000000, 1.000000000000000000, -0.000000000000000000 ) ) ;
#11429=CARTESIAN_POINT ( 'NONE',  ( 0.000000000000000000, 0.1749999999999999889, 0.000000000000000000 ) ) ;
#11442=ORIENTED_EDGE ( 'NONE', *, *, #8733, .F. ) ;
#11466=LINE ( 'NONE', #7800, #11685 ) ;
#11473=CARTESIAN_POINT ( 'NONE',  ( 0.3725000000000000533, 0.1749999999999999889, -0.3724999999999999978 ) ) ;
#11521=CARTESIAN_POINT ( 'NONE',  ( 0.5400755080658357077, 0.1749999999999999889, -1.532626322880899838 ) ) ;
#11523=DIRECTION ( 'NONE',  ( -0.000000000000000000, -1.000000000000000000, 0.000000000000000000 ) ) ;
#11541=DIRECTION ( 'NONE',  ( -0.000000000000000000, -0.000000000000000000, -1.000000000000000000 ) ) ;
#11587=PRODUCT_DEFINITION_FORMATION_WITH_SPECIFIED_SOURCE ( 'ANY', '', #9828, .NOT_KNOWN. ) ;
#11637=DIRECTION ( 'NONE',  ( 0.000000000000000000, -0.000000000000000000, -1.000000000000000000 ) ) ;
#11644=DIRECTION ( 'NONE',  ( 0.000000000000000000, 0.000000000000000000, -1.000000000000000000 ) ) ;
#11660=CARTESIAN_POINT ( 'NONE',  ( 0.7727406610312560487, 0.1749999999999999889, -0.2070552360820117899 ) ) ;
#11668=VERTEX_POINT ( 'NONE', #2344 ) ;
#11675=CARTESIAN_POINT ( 'NONE',  ( 0.8999999999999998002, 0.1549999999999996103, -0.3799999999999999489 ) ) ;
#11677=DIRECTION ( 'NONE',  ( 0.000000000000000000, 0.000000000000000000, -1.000000000000000000 ) ) ;
#11685=VECTOR ( 'NONE', #11541, 39.37007874015748143 ) ;
#11697=ORIENTED_EDGE ( 'NONE', *, *, #10442, .T. ) ;
#11708=CARTESIAN_POINT ( 'NONE',  ( 0.8999999999999998002, 0.000000000000000000, -0.3799999999999999489 ) ) ;
#11709=VECTOR ( 'NONE', #14088, 39.37007874015748143 ) ;
#11712=CIRCLE ( 'NONE', #8060, 0.1250000000000000278 ) ;
#11715=EDGE_CURVE ( 'NONE', #4134, #3613, #2427, .T. ) ;
#11752=DIRECTION ( 'NONE',  ( 0.000000000000000000, 1.000000000000000000, -0.000000000000000000 ) ) ;
#11818=AXIS2_PLACEMENT_3D ( 'NONE', #11473, #972, #14284 ) ;
#11821=EDGE_LOOP ( 'NONE', ( #3392, #211, #244, #7713 ) ) ;
#11825=CLOSED_SHELL ( 'NONE', ( #2341, #10774, #1633, #10533, #10537, #5144, #13462, #7843, #2161, #7457, #2638, #3245, #7647, #939, #9528, #14403, #922, #9148, #743, #6044, #12481, #13173, #2593, #5588, #6895, #2721, #10097 ) ) ;
#11854=FACE_OUTER_BOUND ( 'NONE', #9596, .T. ) ;
#11861=FACE_BOUND ( 'NONE', #8, .T. ) ;
#11879=AXIS2_PLACEMENT_3D ( 'NONE', #5702, #6860, #13349 ) ;
#11892=EDGE_CURVE ( 'NONE', #7601, #12557, #5550, .T. ) ;
#11928=DIRECTION ( 'NONE',  ( 0.000000000000000000, -1.000000000000000000, 0.000000000000000000 ) ) ;
#11982=CARTESIAN_POINT ( 'NONE',  ( 0.5400755080658357077, 0.1749999999999999889, -1.532626322880899838 ) ) ;
#11983=( NAMED_UNIT ( * ) PLANE_ANGLE_UNIT ( ) SI_UNIT ( $, .RADIAN. ) );
#11987=EDGE_LOOP ( 'NONE', ( #10093, #1786, #12415, #10001 ) ) ;
#12042=ORIENTED_EDGE ( 'NONE', *, *, #3207, .F. ) ;
#12108=AXIS2_PLACEMENT_3D ( 'NONE', #7322, #14477, #14559 ) ;
#12116=CARTESIAN_POINT ( 'NONE',  ( 0.4125000000000000333, 0.1749999999999999889, -0.3724999999999999978 ) ) ;
#12129=AXIS2_PLACEMENT_3D ( 'NONE', #14575, #8695, #3956 ) ;
#12139=PRODUCT_CONTEXT ( 'NONE', #1558, 'mechanical' ) ;
#12148=LINE ( 'NONE', #204, #773 ) ;
#12151=VERTEX_POINT ( 'NONE', #2851 ) ;
#12171=AXIS2_PLACEMENT_3D ( 'NONE', #12187, #9604, #14327 ) ;
#12174=AXIS2_PLACEMENT_3D ( 'NONE', #1486, #5095, #9827 ) ;
#12187=CARTESIAN_POINT ( 'NONE',  ( 0.5400755080658357077, 0.1749999999999999889, -1.532626322880899838 ) ) ;
#12194=PLANE ( 'NONE',  #12108 ) ;
#12205=ORIENTED_EDGE ( 'NONE', *, *, #12948, .F. ) ;
#12214=EDGE_CURVE ( 'NONE', #2380, #13228, #8554, .T. ) ;
#12217=DIRECTION ( 'NONE',  ( 0.000000000000000000, 0.000000000000000000, 1.000000000000000000 ) ) ;
#12237=DIRECTION ( 'NONE',  ( -0.000000000000000000, -1.000000000000000000, -0.000000000000000000 ) ) ;
#12250=CARTESIAN_POINT ( 'NONE',  ( 0.4125000000000000333, 0.000000000000000000, -0.4124999999999999778 ) ) ;
#12253=VECTOR ( 'NONE', #13764, 39.37007874015748854 ) ;
#12275=PRODUCT_DEFINITION_CONTEXT ( 'detailed design', #3728, 'design' ) ;
#12278=EDGE_CURVE ( 'NONE', #12557, #616, #6596, .T. ) ;
#12294=EDGE_CURVE ( 'NONE', #1313, #11668, #15063, .T. ) ;
#12295=AXIS2_PLACEMENT_3D ( 'NONE', #10253, #10404, #12755 ) ;
#12310=DIRECTION ( 'NONE',  ( -0.000000000000000000, -1.000000000000000000, 0.000000000000000000 ) ) ;
#12326=( NAMED_UNIT ( * ) SI_UNIT ( $, .STERADIAN. ) SOLID_ANGLE_UNIT ( ) );
#12332=LINE ( 'NONE', #13699, #14287 ) ;
#12334=VECTOR ( 'NONE', #8298, 39.37007874015748143 ) ;
#12341=CARTESIAN_POINT ( 'NONE',  ( 0.9176380235743000213, 0.000000000000000000, -0.1164708448095589793 ) ) ;
#12383=CIRCLE ( 'NONE', #1147, 0.08500000000000004774 ) ;
#12395=ORIENTED_EDGE ( 'NONE', *, *, #260, .F. ) ;
#12415=ORIENTED_EDGE ( 'NONE', *, *, #6160, .F. ) ;
#12425=AXIS2_PLACEMENT_3D ( 'NONE', #11982, #102, #1488 ) ;
#12462=VERTEX_POINT ( 'NONE', #13132 ) ;
#12481=ADVANCED_FACE ( 'NONE', ( #7127 ), #7270, .F. ) ;
#12496=ORIENTED_EDGE ( 'NONE', *, *, #2125, .F. ) ;
#12517=ORIENTED_EDGE ( 'NONE', *, *, #13239, .F. ) ;
#12528=CARTESIAN_POINT ( 'NONE',  ( 0.8999999999999998002, 0.01999999999999975409, -0.3799999999999999489 ) ) ;
#12538=DIRECTION ( 'NONE',  ( -1.000000000000000000, 0.000000000000000000, 0.000000000000000000 ) ) ;
#12557=VERTEX_POINT ( 'NONE', #6410 ) ;
#12567=EDGE_LOOP ( 'NONE', ( #10449, #14754, #5089, #888 ) ) ;
#12589=CARTESIAN_POINT ( 'NONE',  ( 0.3725000000000000533, 0.1749999999999999889, 0.3724999999999999978 ) ) ;
#12591=EDGE_CURVE ( 'NONE', #6934, #11668, #562, .T. ) ;
#12639=DIRECTION ( 'NONE',  ( -0.000000000000000000, -1.000000000000000000, -0.000000000000000000 ) ) ;
#12649=VERTEX_POINT ( 'NONE', #720 ) ;
#12674=EDGE_LOOP ( 'NONE', ( #1951, #11054, #11075, #12395 ) ) ;
#12694=LINE ( 'NONE', #1054, #5842 ) ;
#12697=AXIS2_PLACEMENT_3D ( 'NONE', #11708, #10121, #14774 ) ;
#12699=FACE_OUTER_BOUND ( 'NONE', #1233, .T. ) ;
#12708=EDGE_CURVE ( 'NONE', #7657, #12462, #11712, .T. ) ;
#12723=DIRECTION ( 'NONE',  ( -0.000000000000000000, -1.000000000000000000, -0.000000000000000000 ) ) ;
#12734=DIRECTION ( 'NONE',  ( -0.000000000000000000, -1.000000000000000000, 0.000000000000000000 ) ) ;
#12749=CARTESIAN_POINT ( 'NONE',  ( -0.3724999999999999423, 0.000000000000000000, 0.4124999999999999778 ) ) ;
#12755=DIRECTION ( 'NONE',  ( 0.000000000000000000, 0.000000000000000000, -1.000000000000000000 ) ) ;
#12774=CARTESIAN_POINT ( 'NONE',  ( 0.000000000000000000, 0.1749999999999999889, 0.000000000000000000 ) ) ;
#12788=DIRECTION ( 'NONE',  ( -0.000000000000000000, -1.000000000000000000, -0.000000000000000000 ) ) ;
#12811=AXIS2_PLACEMENT_3D ( 'NONE', #10278, #8899, #5536 ) ;
#12864=DIRECTION ( 'NONE',  ( -0.000000000000000000, 1.000000000000000000, -0.000000000000000000 ) ) ;
#12872=EDGE_CURVE ( 'NONE', #10755, #10245, #13886, .T. ) ;
#12900=DIRECTION ( 'NONE',  ( 0.000000000000000000, 0.000000000000000000, 1.000000000000000000 ) ) ;
#12943=CYLINDRICAL_SURFACE ( 'NONE', #7398, 0.1249999999999999029 ) ;
#12948=EDGE_CURVE ( 'NONE', #12151, #12649, #1436, .T. ) ;
#12949=ORIENTED_EDGE ( 'NONE', *, *, #8733, .T. ) ;
#12950=CARTESIAN_POINT ( 'NONE',  ( 1.650520655410188775, 0.1749999999999999889, -0.5816197779170857451 ) ) ;
#12963=CARTESIAN_POINT ( 'NONE',  ( 0.3725000000000000533, 0.1749999999999999889, -0.4124999999999999778 ) ) ;
#12990=DIRECTION ( 'NONE',  ( 0.000000000000000000, 1.000000000000000000, 0.000000000000000000 ) ) ;
#13024=AXIS2_PLACEMENT_3D ( 'NONE', #2520, #8419, #1280 ) ;
#13027=ORIENTED_EDGE ( 'NONE', *, *, #4633, .F. ) ;
#13037=DIRECTION ( 'NONE',  ( 0.000000000000000000, 1.000000000000000000, -0.000000000000000000 ) ) ;
#13043=EDGE_LOOP ( 'NONE', ( #13103, #7469, #2115, #10565 ) ) ;
#13069=EDGE_LOOP ( 'NONE', ( #9718, #11697 ) ) ;
#13080=DIRECTION ( 'NONE',  ( -0.000000000000000000, 1.000000000000000000, -0.000000000000000000 ) ) ;
#13103=ORIENTED_EDGE ( 'NONE', *, *, #3950, .T. ) ;
#13132=CARTESIAN_POINT ( 'NONE',  ( 1.564978703518703940, 0.000000000000000000, -0.4193347797797316034 ) ) ;
#13166=CARTESIAN_POINT ( 'NONE',  ( -0.3724999999999999423, 0.1749999999999999889, 0.4124999999999999778 ) ) ;
#13173=ADVANCED_FACE ( 'NONE', ( #6005 ), #10670, .F. ) ;
#13194=ORIENTED_EDGE ( 'NONE', *, *, #11715, .F. ) ;
#13228=VERTEX_POINT ( 'NONE', #5298 ) ;
#13239=EDGE_CURVE ( 'NONE', #12151, #2908, #7667, .T. ) ;
#13259=VECTOR ( 'NONE', #12788, 39.37007874015748143 ) ;
#13300=DIRECTION ( 'NONE',  ( 0.000000000000000000, 1.000000000000000000, -0.000000000000000000 ) ) ;
#13309=VECTOR ( 'NONE', #12864, 39.37007874015748143 ) ;
#13315=CARTESIAN_POINT ( 'NONE',  ( 0.000000000000000000, 0.1749999999999999889, 0.000000000000000000 ) ) ;
#13331=CARTESIAN_POINT ( 'NONE',  ( 0.8999999999999998002, 0.1549999999999996103, -0.3799999999999999489 ) ) ;
#13349=DIRECTION ( 'NONE',  ( 0.000000000000000000, 0.000000000000000000, -1.000000000000000000 ) ) ;
#13374=DIRECTION ( 'NONE',  ( 0.000000000000000000, 0.000000000000000000, 1.000000000000000000 ) ) ;
#13387=AXIS2_PLACEMENT_3D ( 'NONE', #10424, #2467, #4690 ) ;
#13400=LINE ( 'NONE', #6535, #9622 ) ;
#13455=CIRCLE ( 'NONE', #492, 0.1050000000000001071 ) ;
#13458=VERTEX_POINT ( 'NONE', #9288 ) ;
#13462=ADVANCED_FACE ( 'NONE', ( #6061, #6988, #1454 ), #143, .F. ) ;
#13482=AXIS2_PLACEMENT_3D ( 'NONE', #10952, #1749, #8589 ) ;
#13522=DIRECTION ( 'NONE',  ( 0.000000000000000000, 0.000000000000000000, 1.000000000000000000 ) ) ;
#13545=CIRCLE ( 'NONE', #100, 0.1250000000000000278 ) ;
#13561=EDGE_CURVE ( 'NONE', #4391, #3525, #14081, .T. ) ;
#13575=CARTESIAN_POINT ( 'NONE',  ( 0.4193347797797013499, 0.000000000000000000, -1.564978703518711711 ) ) ;
#13576=VECTOR ( 'NONE', #8183, 39.37007874015748854 ) ;
#13587=CARTESIAN_POINT ( 'NONE',  ( 0.8999999999999998002, 0.1749999999999999889, -0.2749999999999993006 ) ) ;
#13592=VERTEX_POINT ( 'NONE', #1528 ) ;
#13600=EDGE_CURVE ( 'NONE', #10755, #13592, #585, .T. ) ;
#13606=LINE ( 'NONE', #13831, #3779 ) ;
#13630=ORIENTED_EDGE ( 'NONE', *, *, #3102, .F. ) ;
#13647=ORIENTED_EDGE ( 'NONE', *, *, #1257, .F. ) ;
#13649=VECTOR ( 'NONE', #14720, 39.37007874015748143 ) ;
#13654=CARTESIAN_POINT ( 'NONE',  ( 0.8999999999999998002, 0.1749999999999999889, -0.3799999999999999489 ) ) ;
#13699=CARTESIAN_POINT ( 'NONE',  ( 0.5816197779170538817, 0.1749999999999999889, -1.650520655410200099 ) ) ;
#13746=CARTESIAN_POINT ( 'NONE',  ( 1.532626322880889402, 0.1749999999999999889, -0.5400755080658653506 ) ) ;
#13764=DIRECTION ( 'NONE',  ( 0.9659258262890698665, 0.000000000000000000, -0.2588190451025147443 ) ) ;
#13781=AXIS2_PLACEMENT_3D ( 'NONE', #7266, #14205, #44 ) ;
#13788=EDGE_CURVE ( 'NONE', #13228, #7297, #2818, .T. ) ;
#13831=CARTESIAN_POINT ( 'NONE',  ( 0.8999999999999998002, 0.1749999999999999889, -0.4650000000000000244 ) ) ;
#13847=ORIENTED_EDGE ( 'NONE', *, *, #11892, .F. ) ;
#13885=EDGE_CURVE ( 'NONE', #13592, #3626, #7955, .T. ) ;
#13886=CIRCLE ( 'NONE', #12425, 0.1249999999999999029 ) ;
#13893=ORIENTED_EDGE ( 'NONE', *, *, #5155, .T. ) ;
#13905=CARTESIAN_POINT ( 'NONE',  ( 0.8852856429364857060, 0.1749999999999999889, -0.2372115730956926571 ) ) ;
#13930=ORIENTED_EDGE ( 'NONE', *, *, #5518, .F. ) ;
#14003=ORIENTED_EDGE ( 'NONE', *, *, #8783, .F. ) ;
#14005=FACE_OUTER_BOUND ( 'NONE', #3852, .T. ) ;
#14007=ORIENTED_EDGE ( 'NONE', *, *, #13788, .F. ) ;
#14042=ORIENTED_EDGE ( 'NONE', *, *, #8797, .F. ) ;
#14049=( NAMED_UNIT ( * ) PLANE_ANGLE_UNIT ( ) SI_UNIT ( $, .RADIAN. ) );
#14081=LINE ( 'NONE', #3616, #12334 ) ;
#14088=DIRECTION ( 'NONE',  ( 0.000000000000000000, 1.000000000000000000, 0.000000000000000000 ) ) ;
#14091=PLANE ( 'NONE',  #9675 ) ;
#14101=DIRECTION ( 'NONE',  ( 0.000000000000000000, 0.000000000000000000, -1.000000000000000000 ) ) ;
#14128=ORIENTED_EDGE ( 'NONE', *, *, #14687, .F. ) ;
#14159=ORIENTED_EDGE ( 'NONE', *, *, #2307, .F. ) ;
#14171=ORIENTED_EDGE ( 'NONE', *, *, #2021, .F. ) ;
#14178=DIRECTION ( 'NONE',  ( 1.775701195881770796E-15, 0.000000000000000000, -1.000000000000000000 ) ) ;
#14196=AXIS2_PLACEMENT_3D ( 'NONE', #1634, #3021, #7767 ) ;
#14205=DIRECTION ( 'NONE',  ( -0.000000000000000000, -1.000000000000000000, 0.000000000000000000 ) ) ;
#14206=EDGE_LOOP ( 'NONE', ( #11171, #223, #3769, #14964, #8736, #10820, #7930, #2202 ) ) ;
#14245=DIRECTION ( 'NONE',  ( 0.000000000000000000, 0.000000000000000000, 1.000000000000000000 ) ) ;
#14250=CIRCLE ( 'NONE', #13024, 0.03999999999999998002 ) ;
#14269=DIRECTION ( 'NONE',  ( 0.000000000000000000, -1.000000000000000000, 0.000000000000000000 ) ) ;
#14284=DIRECTION ( 'NONE',  ( 0.000000000000000000, 0.000000000000000000, -1.000000000000000000 ) ) ;
#14287=VECTOR ( 'NONE', #760, 39.37007874015748143 ) ;
#14321=DIRECTION ( 'NONE',  ( -0.000000000000000000, -1.000000000000000000, -0.000000000000000000 ) ) ;
#14325=CARTESIAN_POINT ( 'NONE',  ( 1.532626322880889402, 0.1749999999999999889, -0.5400755080658653506 ) ) ;
#14327=DIRECTION ( 'NONE',  ( 0.000000000000000000, 0.000000000000000000, -1.000000000000000000 ) ) ;
#14329=CIRCLE ( 'NONE', #14822, 0.1249999999999999029 ) ;
#14370=CIRCLE ( 'NONE', #13387, 0.8000000000000000444 ) ;
#14403=ADVANCED_FACE ( 'NONE', ( #1704 ), #12194, .T. ) ;
#14459=CARTESIAN_POINT ( 'NONE',  ( -0.4124999999999999223, 0.1749999999999999889, -0.4124999999999999778 ) ) ;
#14462=VERTEX_POINT ( 'NONE', #12116 ) ;
#14477=DIRECTION ( 'NONE',  ( 0.000000000000000000, 0.000000000000000000, -1.000000000000000000 ) ) ;
#14559=DIRECTION ( 'NONE',  ( -1.000000000000000000, 0.000000000000000000, -0.000000000000000000 ) ) ;
#14560=ORIENTED_EDGE ( 'NONE', *, *, #3207, .T. ) ;
#14575=CARTESIAN_POINT ( 'NONE',  ( 0.8999999999999998002, 0.01999999999999975409, -0.3799999999999999489 ) ) ;
#14584=FACE_OUTER_BOUND ( 'NONE', #2552, .T. ) ;
#14602=CARTESIAN_POINT ( 'NONE',  ( 0.3725000000000000533, 0.000000000000000000, -0.3724999999999999978 ) ) ;
#14626=AXIS2_PLACEMENT_3D ( 'NONE', #7878, #12310, #5513 ) ;
#14628=AXIS2_PLACEMENT_3D ( 'NONE', #9592, #13300, #5071 ) ;
#14649=DIRECTION ( 'NONE',  ( 0.000000000000000000, 0.000000000000000000, -1.000000000000000000 ) ) ;
#14656=VERTEX_POINT ( 'NONE', #1159 ) ;
#14667=CARTESIAN_POINT ( 'NONE',  ( 1.532626322880889402, 0.000000000000000000, -0.5400755080658653506 ) ) ;
#14687=EDGE_CURVE ( 'NONE', #13228, #7657, #4857, .T. ) ;
#14691=DIRECTION ( 'NONE',  ( 0.000000000000000000, 0.000000000000000000, 1.000000000000000000 ) ) ;
#14697=AXIS2_PLACEMENT_3D ( 'NONE', #12341, #4175, #14792 ) ;
#14698=DIRECTION ( 'NONE',  ( 0.000000000000000000, 0.000000000000000000, -1.000000000000000000 ) ) ;
#14720=DIRECTION ( 'NONE',  ( 8.659560562355000651E-17, -0.7071067811865421326, 0.7071067811865530128 ) ) ;
#14734=CARTESIAN_POINT ( 'NONE',  ( 0.2372115730956756152, 0.1749999999999999889, -0.8852856429364902580 ) ) ;
#14754=ORIENTED_EDGE ( 'NONE', *, *, #3172, .T. ) ;
#14764=EDGE_CURVE ( 'NONE', #13458, #12462, #4545, .T. ) ;
#14774=DIRECTION ( 'NONE',  ( 0.000000000000000000, 0.000000000000000000, -1.000000000000000000 ) ) ;
#14790=EDGE_LOOP ( 'NONE', ( #2343, #8284, #10586, #4678 ) ) ;
#14792=DIRECTION ( 'NONE',  ( 1.092739197465705485E-15, 0.000000000000000000, -1.000000000000000000 ) ) ;
#14822=AXIS2_PLACEMENT_3D ( 'NONE', #11521, #4563, #1326 ) ;
#14825=EDGE_LOOP ( 'NONE', ( #1366, #10835, #10045, #14128 ) ) ;
#14919=DIRECTION ( 'NONE',  ( -0.000000000000000000, -1.000000000000000000, -0.000000000000000000 ) ) ;
#14922=ORIENTED_EDGE ( 'NONE', *, *, #5888, .F. ) ;
#14930=EDGE_CURVE ( 'NONE', #3525, #2976, #11102, .T. ) ;
#14950=ORIENTED_EDGE ( 'NONE', *, *, #3355, .F. ) ;
#14964=ORIENTED_EDGE ( 'NONE', *, *, #10391, .T. ) ;
#14988=ORIENTED_EDGE ( 'NONE', *, *, #8522, .F. ) ;
#15055=VERTEX_POINT ( 'NONE', #3454 ) ;
#15063=LINE ( 'NONE', #3596, #8080 ) ;
#15111=LINE ( 'NONE', #7172, #5919 ) ;
#15113=DIRECTION ( 'NONE',  ( -0.000000000000000000, -1.000000000000000000, -0.000000000000000000 ) ) ;
#15119=AXIS2_PLACEMENT_3D ( 'NONE', #1745, #7728, #11166 ) ;
#15129=VERTEX_POINT ( 'NONE', #6981 ) ;
#15136=LENGTH_MEASURE_WITH_UNIT ( LENGTH_MEASURE( 0.02539999999999999897 ), #2978 );
#15200=COLOUR_RGB('Off White',0.89,0.88,0.83);
#15201=FILL_AREA_STYLE_COLOUR('',#15200);
#15202=FILL_AREA_STYLE('',(#15201));
#15203=SURFACE_STYLE_FILL_AREA(#15202);
#15204=SURFACE_SIDE_STYLE('',(#15203));
#15205=SURFACE_STYLE_USAGE(.BOTH.,#15204);
#15206=PRESENTATION_STYLE_ASSIGNMENT((#15205));
ENDSEC;
END-ISO-10303-21;
